ISO-10303-21;
HEADER;
/* Generated by software containing ST-Developer
 * from STEP Tools, Inc. (www.steptools.com) 
 */

FILE_DESCRIPTION(
/* description */ ('STEP AP214'),
/* implementation_level */ '2;1');

FILE_NAME(
/* name */ 'Hex Nut DIN Grade C.step',
/* time_stamp */ '2026-11-14T05:56:09-08:00',
/* author */ (''),
/* organization */ (''),
/* preprocessor_version */ 'ST-DEVELOPER v20.2',
/* originating_system */ 'Autodesk Translation Framework v15.17.0.0',
/* authorisation */ '');

FILE_SCHEMA (('AUTOMOTIVE_DESIGN { 1 0 10303 214 3 1 1 }'));
ENDSEC;

DATA;
#10=MECHANICAL_DESIGN_GEOMETRIC_PRESENTATION_REPRESENTATION('',(#107),#3207);
#71=(
BOUNDED_SURFACE()
B_SPLINE_SURFACE(1,2,((#2712,#2713,#2714,#2715,#2716,#2717,#2718,#2719,
#2720,#2721,#2722,#2723,#2724,#2725,#2726,#2727,#2728,#2729,#2730,#2731,
#2732,#2733,#2734,#2735,#2736,#2737,#2738,#2739,#2740,#2741,#2742,#2743,
#2744,#2745,#2746,#2747,#2748,#2749,#2750,#2751,#2752,#2753,#2754,#2755,
#2756,#2757,#2758,#2759,#2760,#2761,#2762,#2763,#2764,#2765,#2766,#2767,
#2768,#2769,#2770,#2771,#2772,#2773,#2774,#2775,#2776,#2777,#2778,#2779,
#2780,#2781,#2782,#2783,#2784,#2785,#2786,#2787,#2788,#2789,#2790,#2791,
#2792,#2793,#2794,#2795,#2796,#2797,#2798,#2799,#2800,#2801,#2802,#2803,
#2804,#2805,#2806,#2807,#2808),(#2809,#2810,#2811,#2812,#2813,#2814,#2815,
#2816,#2817,#2818,#2819,#2820,#2821,#2822,#2823,#2824,#2825,#2826,#2827,
#2828,#2829,#2830,#2831,#2832,#2833,#2834,#2835,#2836,#2837,#2838,#2839,
#2840,#2841,#2842,#2843,#2844,#2845,#2846,#2847,#2848,#2849,#2850,#2851,
#2852,#2853,#2854,#2855,#2856,#2857,#2858,#2859,#2860,#2861,#2862,#2863,
#2864,#2865,#2866,#2867,#2868,#2869,#2870,#2871,#2872,#2873,#2874,#2875,
#2876,#2877,#2878,#2879,#2880,#2881,#2882,#2883,#2884,#2885,#2886,#2887,
#2888,#2889,#2890,#2891,#2892,#2893,#2894,#2895,#2896,#2897,#2898,#2899,
#2900,#2901,#2902,#2903,#2904,#2905)),.UNSPECIFIED.,.F.,.F.,.F.)
B_SPLINE_SURFACE_WITH_KNOTS((2,2),(3,2,2,2,2,2,2,2,2,2,2,2,2,2,2,2,2,2,
2,2,2,2,2,2,2,2,2,2,2,2,2,2,2,2,2,2,2,2,2,2,2,2,2,2,2,2,2,2,3),(0.,1.),
(0.,0.0208333333333333,0.0416666666666667,0.0625,0.0833333333333333,0.104166666666667,
0.125,0.145833333333333,0.166666666666667,0.1875,0.208333333333333,0.229166666666667,
0.25,0.270833333333333,0.291666666666667,0.3125,0.333333333333333,0.354166666666667,
0.375,0.395833333333333,0.416666666666667,0.4375,0.458333333333333,0.479166666666667,
0.5,0.520833333333333,0.541666666666667,0.5625,0.583333333333333,0.604166666666667,
0.625,0.645833333333333,0.666666666666667,0.6875,0.708333333333333,0.729166666666667,
0.75,0.770833333333333,0.791666666666667,0.8125,0.833333333333333,0.854166666666667,
0.875,0.895833333333333,0.916666666666667,0.9375,0.958333333333333,0.979166666666667,
1.),.UNSPECIFIED.)
GEOMETRIC_REPRESENTATION_ITEM()
RATIONAL_B_SPLINE_SURFACE(((1.,0.923879532511287,1.,0.923879532511287,1.,
0.923879532511287,1.,0.923879532511287,1.,0.923879532511287,1.,0.923879532511287,
1.,0.923879532511287,1.,0.923879532511287,1.,0.923879532511287,1.,0.923879532511287,
1.,0.923879532511287,1.,0.923879532511287,1.,0.923879532511287,1.,0.923879532511287,
1.,0.923879532511287,1.,0.923879532511287,1.,0.923879532511287,1.,0.923879532511287,
1.,0.923879532511287,1.,0.923879532511287,1.,0.923879532511287,1.,0.923879532511287,
1.,0.923879532511287,1.,0.923879532511287,1.,0.923879532511287,1.,0.923879532511287,
1.,0.923879532511287,1.,0.923879532511287,1.,0.923879532511287,1.,0.923879532511287,
1.,0.923879532511287,1.,0.923879532511287,1.,0.923879532511287,1.,0.923879532511287,
1.,0.923879532511287,1.,0.923879532511287,1.,0.923879532511287,1.,0.923879532511287,
1.,0.923879532511287,1.,0.923879532511287,1.,0.923879532511287,1.,0.923879532511287,
1.,0.923879532511287,1.,0.923879532511287,1.,0.923879532511287,1.,0.923879532511287,
1.,0.923879532511287,1.,0.923879532511287,1.),(1.,0.923879532511287,1.,
0.923879532511287,1.,0.923879532511287,1.,0.923879532511287,1.,0.923879532511287,
1.,0.923879532511287,1.,0.923879532511287,1.,0.923879532511287,1.,0.923879532511287,
1.,0.923879532511287,1.,0.923879532511287,1.,0.923879532511287,1.,0.923879532511287,
1.,0.923879532511287,1.,0.923879532511287,1.,0.923879532511287,1.,0.923879532511287,
1.,0.923879532511287,1.,0.923879532511287,1.,0.923879532511287,1.,0.923879532511287,
1.,0.923879532511287,1.,0.923879532511287,1.,0.923879532511287,1.,0.923879532511287,
1.,0.923879532511287,1.,0.923879532511287,1.,0.923879532511287,1.,0.923879532511287,
1.,0.923879532511287,1.,0.923879532511287,1.,0.923879532511287,1.,0.923879532511287,
1.,0.923879532511287,1.,0.923879532511287,1.,0.923879532511287,1.,0.923879532511287,
1.,0.923879532511287,1.,0.923879532511287,1.,0.923879532511287,1.,0.923879532511287,
1.,0.923879532511287,1.,0.923879532511287,1.,0.923879532511287,1.,0.923879532511287,
1.,0.923879532511287,1.,0.923879532511287,1.,0.923879532511287,1.)))
REPRESENTATION_ITEM('')
SURFACE()
);
#72=(
BOUNDED_SURFACE()
B_SPLINE_SURFACE(1,2,((#2983,#2984,#2985,#2986,#2987,#2988,#2989,#2990,
#2991,#2992,#2993,#2994,#2995,#2996,#2997,#2998,#2999,#3000,#3001,#3002,
#3003,#3004,#3005,#3006,#3007,#3008,#3009,#3010,#3011,#3012,#3013,#3014,
#3015,#3016,#3017,#3018,#3019,#3020,#3021,#3022,#3023,#3024,#3025,#3026,
#3027,#3028,#3029,#3030,#3031,#3032,#3033,#3034,#3035,#3036,#3037,#3038,
#3039,#3040,#3041,#3042,#3043,#3044,#3045,#3046,#3047,#3048,#3049,#3050,
#3051,#3052,#3053,#3054,#3055,#3056,#3057,#3058,#3059,#3060,#3061,#3062,
#3063,#3064,#3065,#3066,#3067,#3068,#3069,#3070,#3071,#3072,#3073,#3074,
#3075,#3076,#3077,#3078,#3079),(#3080,#3081,#3082,#3083,#3084,#3085,#3086,
#3087,#3088,#3089,#3090,#3091,#3092,#3093,#3094,#3095,#3096,#3097,#3098,
#3099,#3100,#3101,#3102,#3103,#3104,#3105,#3106,#3107,#3108,#3109,#3110,
#3111,#3112,#3113,#3114,#3115,#3116,#3117,#3118,#3119,#3120,#3121,#3122,
#3123,#3124,#3125,#3126,#3127,#3128,#3129,#3130,#3131,#3132,#3133,#3134,
#3135,#3136,#3137,#3138,#3139,#3140,#3141,#3142,#3143,#3144,#3145,#3146,
#3147,#3148,#3149,#3150,#3151,#3152,#3153,#3154,#3155,#3156,#3157,#3158,
#3159,#3160,#3161,#3162,#3163,#3164,#3165,#3166,#3167,#3168,#3169,#3170,
#3171,#3172,#3173,#3174,#3175,#3176)),.UNSPECIFIED.,.F.,.F.,.F.)
B_SPLINE_SURFACE_WITH_KNOTS((2,2),(3,2,2,2,2,2,2,2,2,2,2,2,2,2,2,2,2,2,
2,2,2,2,2,2,2,2,2,2,2,2,2,2,2,2,2,2,2,2,2,2,2,2,2,2,2,2,2,2,3),(0.,1.00006669780522),
(0.,0.0208333333333333,0.0416666666666667,0.0625,0.0833333333333333,0.104166666666667,
0.125,0.145833333333333,0.166666666666667,0.1875,0.208333333333333,0.229166666666667,
0.25,0.270833333333333,0.291666666666667,0.3125,0.333333333333333,0.354166666666667,
0.375,0.395833333333333,0.416666666666667,0.4375,0.458333333333333,0.479166666666667,
0.5,0.520833333333333,0.541666666666667,0.5625,0.583333333333333,0.604166666666667,
0.625,0.645833333333333,0.666666666666667,0.6875,0.708333333333333,0.729166666666667,
0.75,0.770833333333333,0.791666666666667,0.8125,0.833333333333333,0.854166666666667,
0.875,0.895833333333333,0.916666666666667,0.9375,0.958333333333333,0.979166666666667,
1.),.UNSPECIFIED.)
GEOMETRIC_REPRESENTATION_ITEM()
RATIONAL_B_SPLINE_SURFACE(((1.,0.923879532511287,1.,0.923879532511287,1.,
0.923879532511287,1.,0.923879532511287,1.,0.923879532511287,1.,0.923879532511287,
1.,0.923879532511287,1.,0.923879532511287,1.,0.923879532511287,1.,0.923879532511287,
1.,0.923879532511287,1.,0.923879532511287,1.,0.923879532511287,1.,0.923879532511287,
1.,0.923879532511287,1.,0.923879532511287,1.,0.923879532511287,1.,0.923879532511287,
1.,0.923879532511287,1.,0.923879532511287,1.,0.923879532511287,1.,0.923879532511287,
1.,0.923879532511287,1.,0.923879532511287,1.,0.923879532511287,1.,0.923879532511287,
1.,0.923879532511287,1.,0.923879532511287,1.,0.923879532511287,1.,0.923879532511287,
1.,0.923879532511287,1.,0.923879532511287,1.,0.923879532511287,1.,0.923879532511287,
1.,0.923879532511287,1.,0.923879532511287,1.,0.923879532511287,1.,0.923879532511287,
1.,0.923879532511287,1.,0.923879532511287,1.,0.923879532511287,1.,0.923879532511287,
1.,0.923879532511287,1.,0.923879532511287,1.,0.923879532511287,1.,0.923879532511287,
1.,0.923879532511287,1.,0.923879532511287,1.),(1.,0.923879532511287,1.,
0.923879532511287,1.,0.923879532511287,1.,0.923879532511287,1.,0.923879532511287,
1.,0.923879532511287,1.,0.923879532511287,1.,0.923879532511287,1.,0.923879532511287,
1.,0.923879532511287,1.,0.923879532511287,1.,0.923879532511287,1.,0.923879532511287,
1.,0.923879532511287,1.,0.923879532511287,1.,0.923879532511287,1.,0.923879532511287,
1.,0.923879532511287,1.,0.923879532511287,1.,0.923879532511287,1.,0.923879532511287,
1.,0.923879532511287,1.,0.923879532511287,1.,0.923879532511287,1.,0.923879532511287,
1.,0.923879532511287,1.,0.923879532511287,1.,0.923879532511287,1.,0.923879532511287,
1.,0.923879532511287,1.,0.923879532511287,1.,0.923879532511287,1.,0.923879532511287,
1.,0.923879532511287,1.,0.923879532511287,1.,0.923879532511287,1.,0.923879532511287,
1.,0.923879532511287,1.,0.923879532511287,1.,0.923879532511287,1.,0.923879532511287,
1.,0.923879532511287,1.,0.923879532511287,1.,0.923879532511287,1.,0.923879532511287,
1.,0.923879532511287,1.,0.923879532511287,1.,0.923879532511287,1.)))
REPRESENTATION_ITEM('')
SURFACE()
);
#73=(
BOUNDED_CURVE()
B_SPLINE_CURVE(2,(#2576,#2577,#2578),.UNSPECIFIED.,.F.,.F.)
B_SPLINE_CURVE_WITH_KNOTS((3,3),(-2.54218368144079,-1.15030563525544),
 .UNSPECIFIED.)
CURVE()
GEOMETRIC_REPRESENTATION_ITEM()
RATIONAL_B_SPLINE_CURVE((1.87625870439026,2.16651693610016,1.87625870439027))
REPRESENTATION_ITEM('')
);
#74=(
BOUNDED_CURVE()
B_SPLINE_CURVE(2,(#2580,#2581,#2582),.UNSPECIFIED.,.F.,.F.)
B_SPLINE_CURVE_WITH_KNOTS((3,3),(-2.54218475501031,-1.15030626839472),
 .UNSPECIFIED.)
CURVE()
GEOMETRIC_REPRESENTATION_ITEM()
RATIONAL_B_SPLINE_CURVE((1.87625926314051,2.16651758128937,1.87625926314051))
REPRESENTATION_ITEM('')
);
#75=(
BOUNDED_CURVE()
B_SPLINE_CURVE(2,(#2584,#2585,#2586),.UNSPECIFIED.,.F.,.F.)
B_SPLINE_CURVE_WITH_KNOTS((3,3),(-2.54218368144076,-1.15030563525543),
 .UNSPECIFIED.)
CURVE()
GEOMETRIC_REPRESENTATION_ITEM()
RATIONAL_B_SPLINE_CURVE((1.87625870439026,2.16651693610015,1.87625870439025))
REPRESENTATION_ITEM('')
);
#76=(
BOUNDED_CURVE()
B_SPLINE_CURVE(2,(#2589,#2590,#2591),.UNSPECIFIED.,.F.,.F.)
B_SPLINE_CURVE_WITH_KNOTS((3,3),(1.15030563525545,2.54218368144079),
 .UNSPECIFIED.)
CURVE()
GEOMETRIC_REPRESENTATION_ITEM()
RATIONAL_B_SPLINE_CURVE((1.87625870439026,2.16651693610015,1.87625870439025))
REPRESENTATION_ITEM('')
);
#77=(
BOUNDED_CURVE()
B_SPLINE_CURVE(2,(#2593,#2594,#2595),.UNSPECIFIED.,.F.,.F.)
B_SPLINE_CURVE_WITH_KNOTS((3,3),(1.15030626839473,2.54218475501033),
 .UNSPECIFIED.)
CURVE()
GEOMETRIC_REPRESENTATION_ITEM()
RATIONAL_B_SPLINE_CURVE((1.87625926314051,2.16651758128937,1.8762592631405))
REPRESENTATION_ITEM('')
);
#78=(
BOUNDED_CURVE()
B_SPLINE_CURVE(2,(#2596,#2597,#2598),.UNSPECIFIED.,.F.,.F.)
B_SPLINE_CURVE_WITH_KNOTS((3,3),(1.15030563525543,2.54218368144081),
 .UNSPECIFIED.)
CURVE()
GEOMETRIC_REPRESENTATION_ITEM()
RATIONAL_B_SPLINE_CURVE((1.87625870439027,2.16651693610019,1.87625870439027))
REPRESENTATION_ITEM('')
);
#79=(
BOUNDED_CURVE()
B_SPLINE_CURVE(2,(#2602,#2603,#2604),.UNSPECIFIED.,.F.,.F.)
B_SPLINE_CURVE_WITH_KNOTS((3,3),(-2.66143679957435,-1.22056556713595),
 .UNSPECIFIED.)
CURVE()
GEOMETRIC_REPRESENTATION_ITEM()
RATIONAL_B_SPLINE_CURVE((1.93841739578654,2.23829161052161,1.93841739578655))
REPRESENTATION_ITEM('')
);
#80=(
BOUNDED_CURVE()
B_SPLINE_CURVE(2,(#2606,#2607,#2608),.UNSPECIFIED.,.F.,.F.)
B_SPLINE_CURVE_WITH_KNOTS((3,3),(-2.66143679957435,-1.22056556713593),
 .UNSPECIFIED.)
CURVE()
GEOMETRIC_REPRESENTATION_ITEM()
RATIONAL_B_SPLINE_CURVE((1.93841739578655,2.23829161052162,1.93841739578654))
REPRESENTATION_ITEM('')
);
#81=(
BOUNDED_CURVE()
B_SPLINE_CURVE(2,(#2610,#2611,#2612),.UNSPECIFIED.,.F.,.F.)
B_SPLINE_CURVE_WITH_KNOTS((3,3),(-2.66143679957436,-1.22056556713593),
 .UNSPECIFIED.)
CURVE()
GEOMETRIC_REPRESENTATION_ITEM()
RATIONAL_B_SPLINE_CURVE((1.93841739578655,2.23829161052163,1.93841739578654))
REPRESENTATION_ITEM('')
);
#82=(
BOUNDED_CURVE()
B_SPLINE_CURVE(2,(#2615,#2616,#2617),.UNSPECIFIED.,.F.,.F.)
B_SPLINE_CURVE_WITH_KNOTS((3,3),(1.22056556713593,2.66143679957439),
 .UNSPECIFIED.)
CURVE()
GEOMETRIC_REPRESENTATION_ITEM()
RATIONAL_B_SPLINE_CURVE((1.93841739578656,2.23829161052165,1.93841739578656))
REPRESENTATION_ITEM('')
);
#83=(
BOUNDED_CURVE()
B_SPLINE_CURVE(2,(#2619,#2620,#2621),.UNSPECIFIED.,.F.,.F.)
B_SPLINE_CURVE_WITH_KNOTS((3,3),(1.22056556713592,2.66143679957436),
 .UNSPECIFIED.)
CURVE()
GEOMETRIC_REPRESENTATION_ITEM()
RATIONAL_B_SPLINE_CURVE((1.93841739578654,2.23829161052163,1.93841739578655))
REPRESENTATION_ITEM('')
);
#84=(
BOUNDED_CURVE()
B_SPLINE_CURVE(2,(#2622,#2623,#2624),.UNSPECIFIED.,.F.,.F.)
B_SPLINE_CURVE_WITH_KNOTS((3,3),(1.22056556713592,2.66143679957434),
 .UNSPECIFIED.)
CURVE()
GEOMETRIC_REPRESENTATION_ITEM()
RATIONAL_B_SPLINE_CURVE((1.93841739578653,2.23829161052161,1.93841739578655))
REPRESENTATION_ITEM('')
);
#85=(
BOUNDED_CURVE()
B_SPLINE_CURVE(2,(#2906,#2907,#2908,#2909,#2910,#2911,#2912,#2913,#2914,
#2915,#2916,#2917,#2918,#2919,#2920,#2921,#2922,#2923,#2924,#2925,#2926,
#2927,#2928,#2929,#2930,#2931,#2932,#2933,#2934,#2935,#2936,#2937,#2938,
#2939,#2940,#2941,#2942,#2943,#2944,#2945,#2946,#2947,#2948,#2949,#2950,
#2951,#2952,#2953,#2954,#2955,#2956,#2957,#2958,#2959,#2960,#2961,#2962,
#2963,#2964,#2965,#2966,#2967,#2968,#2969,#2970,#2971,#2972,#2973,#2974,
#2975,#2976,#2977,#2978,#2979,#2980,#2981,#2982),.UNSPECIFIED.,.F.,.F.)
B_SPLINE_CURVE_WITH_KNOTS((3,2,2,2,2,2,2,2,2,2,2,2,2,2,2,2,2,2,2,2,2,2,
2,2,2,2,2,2,2,2,2,2,2,2,2,2,2,2,3),(0.0966194075737784,0.104166666666667,
0.125,0.145833333333333,0.166666666666667,0.1875,0.208333333333333,0.229166666666667,
0.25,0.270833333333333,0.291666666666667,0.3125,0.333333333333333,0.354166666666667,
0.375,0.395833333333333,0.416666666666667,0.4375,0.458333333333333,0.479166666666667,
0.5,0.520833333333333,0.541666666666667,0.5625,0.583333333333333,0.604166666666667,
0.625,0.645833333333333,0.666666666666667,0.6875,0.708333333333333,0.729166666666667,
0.75,0.770833333333333,0.791666666666667,0.8125,0.833333333333333,0.854166666666667,
0.868477508058086),.UNSPECIFIED.)
CURVE()
GEOMETRIC_REPRESENTATION_ITEM()
RATIONAL_B_SPLINE_CURVE((0.964827774294736,0.972423957260363,1.,0.923879532511287,
1.,0.923879532511287,1.,0.923879532511287,1.,0.923879532511287,1.,0.923879532511287,
1.,0.923879532511287,1.,0.923879532511287,1.,0.923879532511287,1.,0.923879532511287,
1.,0.923879532511287,1.,0.923879532511287,1.,0.923879532511287,1.,0.923879532511287,
1.,0.923879532511287,1.,0.923879532511287,1.,0.923879532511287,1.,0.923879532511287,
1.,0.923879532511287,1.,0.923879532511287,1.,0.923879532511287,1.,0.923879532511287,
1.,0.923879532511287,1.,0.923879532511287,1.,0.923879532511287,1.,0.923879532511287,
1.,0.923879532511287,1.,0.923879532511287,1.,0.923879532511287,1.,0.923879532511287,
1.,0.923879532511287,1.,0.923879532511287,1.,0.923879532511287,1.,0.923879532511287,
1.,0.923879532511287,1.,0.923879532511287,1.,0.923879532511287,1.,0.94771129903016,
0.967258947450023))
REPRESENTATION_ITEM('')
);
#86=CONICAL_SURFACE('',#1490,3.4,0.785398163397449);
#87=CONICAL_SURFACE('',#1491,4.1,0.785398163397447);
#88=CONICAL_SURFACE('',#1492,5.62820323027547,1.07685495787532);
#89=CONICAL_SURFACE('',#1493,6.92820323027547,1.07685495787532);
#95=SHAPE_REPRESENTATION_RELATIONSHIP('SRR','None',#3247,#101);
#101=ADVANCED_BREP_SHAPE_REPRESENTATION('',(#113),#3206);
#107=STYLED_ITEM('',(#3283),#113);
#113=MANIFOLD_SOLID_BREP('Body1',#1285);
#144=PLANE('',#1495);
#145=PLANE('',#1496);
#146=PLANE('',#1497);
#147=PLANE('',#1498);
#148=PLANE('',#1499);
#149=PLANE('',#1500);
#150=PLANE('',#1501);
#151=PLANE('',#1502);
#208=LINE('',#2204,#275);
#209=LINE('',#2283,#276);
#210=LINE('',#2359,#277);
#211=LINE('',#2587,#278);
#212=LINE('',#2613,#279);
#213=LINE('',#2701,#280);
#214=LINE('',#2702,#281);
#215=LINE('',#2704,#282);
#216=LINE('',#2706,#283);
#217=LINE('',#2708,#284);
#218=LINE('',#2710,#285);
#275=VECTOR('',#1802,3.4);
#276=VECTOR('',#1807,3.4);
#277=VECTOR('',#1810,3.4);
#278=VECTOR('',#1857,5.62820323027547);
#279=VECTOR('',#1860,6.92820323027547);
#280=VECTOR('',#1869,1000.);
#281=VECTOR('',#1870,1000.);
#282=VECTOR('',#1873,1000.);
#283=VECTOR('',#1876,1000.);
#284=VECTOR('',#1879,1000.);
#285=VECTOR('',#1882,1000.);
#305=CYLINDRICAL_SURFACE('',#1466,3.4);
#306=CYLINDRICAL_SURFACE('',#1468,3.4);
#307=CYLINDRICAL_SURFACE('',#1469,3.4);
#308=CYLINDRICAL_SURFACE('',#1494,3.4);
#326=FACE_BOUND('',#506,.T.);
#327=FACE_BOUND('',#508,.T.);
#330=B_SPLINE_CURVE_WITH_KNOTS('',3,(#2206,#2207,#2208,#2209,#2210,#2211,
#2212,#2213,#2214,#2215,#2216,#2217,#2218,#2219,#2220,#2221,#2222,#2223,
#2224,#2225,#2226,#2227,#2228,#2229,#2230,#2231,#2232,#2233,#2234,#2235,
#2236,#2237,#2238,#2239,#2240,#2241),.UNSPECIFIED.,.F.,.F.,(4,2,2,2,2,2,
2,2,2,2,2,2,2,2,2,2,2,4),(-2.10359968512681,-2.08103107378187,-1.94554547637383,
-1.81489062645829,-1.67930255990407,-1.54858519329573,-1.4128945990498,
-1.28211064575253,-1.14631742275592,-1.01546315460342,-0.879567162984071,
-0.748639172872498,-0.612640237993188,-0.481635418621005,-0.345533335297706,
-0.214448857835685,-0.107555631958328,-1.00000006098E-6),.UNSPECIFIED.);
#331=B_SPLINE_CURVE_WITH_KNOTS('',3,(#2244,#2245,#2246,#2247,#2248,#2249,
#2250,#2251,#2252,#2253,#2254,#2255,#2256,#2257,#2258,#2259,#2260,#2261,
#2262,#2263,#2264,#2265,#2266,#2267,#2268,#2269,#2270,#2271,#2272,#2273,
#2274,#2275,#2276,#2277,#2278,#2279),.UNSPECIFIED.,.F.,.F.,(4,2,2,2,2,2,
2,2,2,2,2,2,2,2,2,2,2,4),(-7.85905825298031,-7.77422257041908,-7.68856054816734,
-7.55762981443557,-7.42483713253212,-7.29377710370425,-7.16107861802676,
-7.02988205164815,-6.89727499829573,-6.76593520312556,-6.63341646303585,
-6.50192733294177,-6.36949343700113,-6.23784947539028,-6.10549661518781,
-5.97369294985523,-5.84141699375484,-5.75028258696816),.UNSPECIFIED.);
#332=B_SPLINE_CURVE_WITH_KNOTS('',3,(#2284,#2285,#2286,#2287,#2288,#2289,
#2290,#2291,#2292,#2293,#2294,#2295,#2296,#2297,#2298,#2299,#2300,#2301,
#2302,#2303,#2304,#2305,#2306,#2307,#2308,#2309,#2310,#2311,#2312,#2313,
#2314,#2315,#2316,#2317,#2318,#2319),.UNSPECIFIED.,.F.,.F.,(4,2,2,2,2,2,
2,2,2,2,2,2,2,2,2,2,2,4),(-4.24214101358173,-4.2048914410257,-4.0725209662614,
-3.93981233390169,-3.80504628747379,-3.67468269995894,-3.53981327635047,
-3.40942661287122,-3.27445407429178,-3.14403745333268,-3.00896202440863,
-2.87850898785149,-2.74333084956052,-2.61283536277767,-2.47755464868551,
-2.34701109546997,-2.21162788996109,-2.10359968512681),.UNSPECIFIED.);
#333=B_SPLINE_CURVE_WITH_KNOTS('',3,(#2320,#2321,#2322,#2323,#2324,#2325,
#2326,#2327,#2328,#2329,#2330,#2331,#2332,#2333,#2334,#2335,#2336,#2337,
#2338,#2339,#2340,#2341,#2342,#2343,#2344,#2345,#2346,#2347,#2348,#2349,
#2350,#2351,#2352,#2353,#2354,#2355),.UNSPECIFIED.,.F.,.F.,(4,2,2,2,2,2,
2,2,2,2,2,2,2,2,2,2,2,4),(-5.75028258696816,-5.70944938231978,-5.5772458963651,
-5.44511072272886,-5.31297499576572,-5.18066925825091,-5.04859633055591,
-4.91611762256936,-4.78410231721224,-4.65144880140821,-4.51948575755063,
-4.38665613455588,-4.25473984189617,-4.12173331469736,-3.9869206349123,
-3.85673226776102,-3.72181712106248,-3.61699531260759),.UNSPECIFIED.);
#334=B_SPLINE_CURVE_WITH_KNOTS('',3,(#2361,#2362,#2363,#2364,#2365,#2366,
#2367,#2368,#2369,#2370,#2371,#2372,#2373,#2374,#2375,#2376,#2377,#2378,
#2379,#2380,#2381,#2382,#2383,#2384,#2385,#2386),.UNSPECIFIED.,.F.,.F.,
(4,2,2,2,2,2,2,2,2,2,2,2,4),(-1.47913833354922,-1.46458034294253,-1.32874299195507,
-1.19791685147926,-1.06197629089818,-0.931067644878991,-0.795023617953509,
-0.664030178278347,-0.527882410827952,-0.396802102620113,-0.260550306708762,
-0.129381249781886,0.),.UNSPECIFIED.);
#335=B_SPLINE_CURVE_WITH_KNOTS('',3,(#2389,#2390,#2391,#2392,#2393,#2394,
#2395,#2396,#2397,#2398,#2399,#2400,#2401,#2402,#2403,#2404,#2405,#2406,
#2407,#2408,#2409,#2410,#2411,#2412,#2413,#2414),.UNSPECIFIED.,.F.,.F.,
(4,2,2,2,2,2,2,2,2,2,2,2,4),(-7.86794629923482,-7.75493027201567,-7.64410086775257,
-7.51059875662567,-7.37975989227452,-7.24636016292494,-7.11541902959003,
-6.98212034736466,-6.85106811014228,-6.71786884131222,-6.58669715245899,
-6.45359533086519,-6.3781872802266),.UNSPECIFIED.);
#336=B_SPLINE_CURVE_WITH_KNOTS('',3,(#2434,#2435,#2436,#2437,#2438,#2439,
#2440,#2441,#2442,#2443),.UNSPECIFIED.,.F.,.F.,(4,2,2,2,4),(-0.0148421019360754,
-0.00739951306522483,-0.00292666249453577,-0.00127970164740186,-9.99986987752639E-7),
 .UNSPECIFIED.);
#337=B_SPLINE_CURVE_WITH_KNOTS('',3,(#2445,#2446,#2447,#2448,#2449,#2450),
 .UNSPECIFIED.,.F.,.F.,(4,2,4),(-0.180846840101061,-0.090528276541627,0.),
 .UNSPECIFIED.);
#338=B_SPLINE_CURVE_WITH_KNOTS('',3,(#2463,#2464,#2465,#2466,#2467,#2468,
#2469,#2470,#2471,#2472),.UNSPECIFIED.,.F.,.F.,(4,2,2,2,4),(-0.0149535669506096,
-0.00745287259980322,-0.00294348211124755,-0.00128449704857332,-9.9998565003534E-7),
 .UNSPECIFIED.);
#339=B_SPLINE_CURVE_WITH_KNOTS('',3,(#2474,#2475,#2476,#2477,#2478,#2479),
 .UNSPECIFIED.,.F.,.F.,(4,2,4),(-0.175510513051521,-0.0877546644588136,
0.),.UNSPECIFIED.);
#340=B_SPLINE_CURVE_WITH_KNOTS('',3,(#2482,#2483,#2484,#2485,#2486,#2487,
#2488,#2489,#2490,#2491,#2492,#2493,#2494,#2495,#2496,#2497,#2498,#2499,
#2500,#2501,#2502,#2503,#2504,#2505,#2506,#2507,#2508,#2509,#2510,#2511,
#2512,#2513,#2514,#2515,#2516,#2517,#2518,#2519),.UNSPECIFIED.,.F.,.F.,
(4,2,2,2,2,2,2,2,2,2,2,2,2,2,2,2,2,2,4),(-2.13108149573488,-1.98745320394869,
-1.82962548528831,-1.75200556231172,-1.60034896227162,-1.52279658772495,
-1.44711497528505,-1.29911129776284,-1.22404068635087,-1.08179010710472,
-1.0085761418628,-0.861083913552298,-0.717667486586238,-0.573740353327516,
-0.434041348236743,-0.293705087973695,-0.157727772352155,-0.077033910772711,
-9.99999999695689E-7),.UNSPECIFIED.);
#341=B_SPLINE_CURVE_WITH_KNOTS('',3,(#2520,#2521,#2522,#2523,#2524,#2525,
#2526),.UNSPECIFIED.,.F.,.F.,(4,3,4),(7.22896027101832E-5,0.000673496122850043,
0.000922700028579017),.UNSPECIFIED.);
#342=B_SPLINE_CURVE_WITH_KNOTS('',3,(#2528,#2529,#2530,#2531,#2532,#2533,
#2534,#2535,#2536,#2537,#2538,#2539,#2540,#2541,#2542,#2543,#2544,#2545,
#2546,#2547,#2548,#2549,#2550,#2551,#2552,#2553,#2554,#2555,#2556,#2557,
#2558,#2559,#2560,#2561,#2562,#2563,#2564,#2565),.UNSPECIFIED.,.F.,.F.,
(4,2,2,2,2,2,2,2,2,2,2,2,2,2,2,2,2,2,4),(-2.29340180701325,-2.11049201367315,
-1.93667869438381,-1.74180997494295,-1.56431695471365,-1.39962964819881,
-1.32507267661721,-1.18000971802147,-1.10543583249726,-0.962600865033504,
-0.814892434644476,-0.675985071317851,-0.531921231285643,-0.396796501805424,
-0.327537591697273,-0.257520735009541,-0.126772402545597,-0.0643607479537848,
0.),.UNSPECIFIED.);
#343=B_SPLINE_CURVE_WITH_KNOTS('',3,(#2566,#2567,#2568,#2569,#2570,#2571,
#2572),.UNSPECIFIED.,.F.,.F.,(4,3,4),(7.245944684394E-5,0.000594859777658842,
0.000926310213851899),.UNSPECIFIED.);
#344=B_SPLINE_CURVE_WITH_KNOTS('',3,(#2626,#2627,#2628,#2629,#2630,#2631,
#2632,#2633,#2634,#2635,#2636,#2637,#2638,#2639,#2640,#2641,#2642,#2643,
#2644,#2645,#2646,#2647,#2648,#2649,#2650,#2651,#2652,#2653,#2654,#2655,
#2656,#2657,#2658,#2659,#2660,#2661),.UNSPECIFIED.,.F.,.F.,(4,2,2,2,2,2,
2,2,2,2,2,2,2,2,2,2,2,4),(-6.3781872802266,-6.32229624691882,-6.18928947170399,
-6.05785556861833,-5.92494126266469,-5.79336572062519,-5.66054086162208,
-5.52881738788514,-5.39607860064442,-5.26420150715983,-5.13154507277188,
-4.99950929385351,-4.86693116428519,-4.73473226477145,-4.60222808246359,
-4.46986225672851,-4.33742737861098,-4.24214101358173),.UNSPECIFIED.);
#345=B_SPLINE_CURVE_WITH_KNOTS('',3,(#2662,#2663,#2664,#2665,#2666,#2667,
#2668,#2669,#2670,#2671,#2672,#2673,#2674,#2675,#2676,#2677,#2678,#2679,
#2680,#2681,#2682,#2683,#2684,#2685,#2686,#2687,#2688,#2689,#2690,#2691,
#2692,#2693,#2694,#2695,#2696,#2697),.UNSPECIFIED.,.F.,.F.,(4,2,2,2,2,2,
2,2,2,2,2,2,2,2,2,2,2,4),(-3.61699531260759,-3.59158532582943,-3.45656783651849,
-3.32628708491561,-3.19116732808102,-3.06083249774886,-2.92561049944977,
-2.79521686028228,-2.6598925990378,-2.52943579674619,-2.39400920604108,
-2.26348524364329,-2.12795621518432,-1.99736143304626,-1.86172982053373,
-1.73106087551919,-1.59532649873018,-1.47913833354922),.UNSPECIFIED.);
#400=FACE_OUTER_BOUND('',#493,.T.);
#401=FACE_OUTER_BOUND('',#494,.T.);
#402=FACE_OUTER_BOUND('',#495,.T.);
#403=FACE_OUTER_BOUND('',#496,.T.);
#404=FACE_OUTER_BOUND('',#497,.T.);
#405=FACE_OUTER_BOUND('',#498,.T.);
#406=FACE_OUTER_BOUND('',#499,.T.);
#407=FACE_OUTER_BOUND('',#500,.T.);
#408=FACE_OUTER_BOUND('',#501,.T.);
#409=FACE_OUTER_BOUND('',#502,.T.);
#410=FACE_OUTER_BOUND('',#503,.T.);
#411=FACE_OUTER_BOUND('',#504,.T.);
#412=FACE_OUTER_BOUND('',#505,.T.);
#413=FACE_OUTER_BOUND('',#507,.T.);
#414=FACE_OUTER_BOUND('',#509,.T.);
#415=FACE_OUTER_BOUND('',#510,.T.);
#416=FACE_OUTER_BOUND('',#511,.T.);
#417=FACE_OUTER_BOUND('',#512,.T.);
#418=FACE_OUTER_BOUND('',#513,.T.);
#419=FACE_OUTER_BOUND('',#514,.T.);
#420=FACE_OUTER_BOUND('',#515,.T.);
#421=FACE_OUTER_BOUND('',#516,.T.);
#493=EDGE_LOOP('',(#1081,#1082,#1083,#1084));
#494=EDGE_LOOP('',(#1085,#1086,#1087,#1088));
#495=EDGE_LOOP('',(#1089,#1090,#1091,#1092));
#496=EDGE_LOOP('',(#1093,#1094,#1095,#1096,#1097));
#497=EDGE_LOOP('',(#1098,#1099,#1100,#1101));
#498=EDGE_LOOP('',(#1102,#1103,#1104,#1105,#1106,#1107,#1108));
#499=EDGE_LOOP('',(#1109,#1110,#1111,#1112,#1113,#1114,#1115));
#500=EDGE_LOOP('',(#1116,#1117,#1118,#1119,#1120));
#501=EDGE_LOOP('',(#1121,#1122,#1123,#1124,#1125));
#502=EDGE_LOOP('',(#1126,#1127,#1128,#1129,#1130,#1131,#1132,#1133,#1134));
#503=EDGE_LOOP('',(#1135,#1136,#1137,#1138,#1139,#1140,#1141,#1142,#1143,
#1144));
#504=EDGE_LOOP('',(#1145,#1146,#1147,#1148));
#505=EDGE_LOOP('',(#1149));
#506=EDGE_LOOP('',(#1150));
#507=EDGE_LOOP('',(#1151));
#508=EDGE_LOOP('',(#1152));
#509=EDGE_LOOP('',(#1153,#1154,#1155,#1156));
#510=EDGE_LOOP('',(#1157,#1158,#1159,#1160));
#511=EDGE_LOOP('',(#1161,#1162,#1163,#1164));
#512=EDGE_LOOP('',(#1165,#1166,#1167,#1168));
#513=EDGE_LOOP('',(#1169,#1170,#1171,#1172));
#514=EDGE_LOOP('',(#1173,#1174,#1175,#1176));
#515=EDGE_LOOP('',(#1177,#1178,#1179,#1180,#1181,#1182,#1183,#1184,#1185));
#516=EDGE_LOOP('',(#1186,#1187,#1188,#1189,#1190,#1191,#1192,#1193,#1194));
#569=CIRCLE('',#1467,3.4);
#570=CIRCLE('',#1470,3.4);
#571=CIRCLE('',#1472,5.5021444402588);
#572=CIRCLE('',#1473,0.5);
#573=CIRCLE('',#1474,5.73919435177631);
#574=CIRCLE('',#1475,5.73919435177631);
#575=CIRCLE('',#1477,5.73919435177631);
#576=CIRCLE('',#1478,0.5);
#577=CIRCLE('',#1479,5.5021444402588);
#578=CIRCLE('',#1481,3.95355339059327);
#579=CIRCLE('',#1482,3.95355339059327);
#580=CIRCLE('',#1483,0.5);
#581=CIRCLE('',#1484,4.30710678118655);
#582=CIRCLE('',#1486,4.30710678118655);
#583=CIRCLE('',#1487,0.5);
#584=CIRCLE('',#1488,3.95355339059327);
#585=CIRCLE('',#1489,3.95355339059327);
#657=VERTEX_POINT('',#2202);
#658=VERTEX_POINT('',#2203);
#659=VERTEX_POINT('',#2205);
#660=VERTEX_POINT('',#2242);
#661=VERTEX_POINT('',#2281);
#662=VERTEX_POINT('',#2282);
#663=VERTEX_POINT('',#2357);
#664=VERTEX_POINT('',#2358);
#665=VERTEX_POINT('',#2360);
#666=VERTEX_POINT('',#2387);
#667=VERTEX_POINT('',#2416);
#668=VERTEX_POINT('',#2418);
#669=VERTEX_POINT('',#2420);
#670=VERTEX_POINT('',#2424);
#671=VERTEX_POINT('',#2426);
#672=VERTEX_POINT('',#2430);
#673=VERTEX_POINT('',#2431);
#674=VERTEX_POINT('',#2433);
#675=VERTEX_POINT('',#2444);
#676=VERTEX_POINT('',#2452);
#677=VERTEX_POINT('',#2456);
#678=VERTEX_POINT('',#2458);
#679=VERTEX_POINT('',#2460);
#680=VERTEX_POINT('',#2462);
#681=VERTEX_POINT('',#2473);
#682=VERTEX_POINT('',#2574);
#683=VERTEX_POINT('',#2575);
#684=VERTEX_POINT('',#2579);
#685=VERTEX_POINT('',#2583);
#686=VERTEX_POINT('',#2588);
#687=VERTEX_POINT('',#2592);
#688=VERTEX_POINT('',#2600);
#689=VERTEX_POINT('',#2601);
#690=VERTEX_POINT('',#2605);
#691=VERTEX_POINT('',#2609);
#692=VERTEX_POINT('',#2614);
#693=VERTEX_POINT('',#2618);
#804=EDGE_CURVE('',#657,#658,#208,.T.);
#805=EDGE_CURVE('',#658,#659,#330,.T.);
#806=EDGE_CURVE('',#659,#660,#569,.T.);
#807=EDGE_CURVE('',#657,#660,#331,.F.);
#808=EDGE_CURVE('',#661,#662,#209,.T.);
#809=EDGE_CURVE('',#662,#658,#332,.T.);
#810=EDGE_CURVE('',#661,#657,#333,.F.);
#811=EDGE_CURVE('',#663,#664,#210,.T.);
#812=EDGE_CURVE('',#665,#663,#334,.F.);
#813=EDGE_CURVE('',#665,#666,#570,.T.);
#814=EDGE_CURVE('',#666,#664,#335,.T.);
#815=EDGE_CURVE('',#667,#667,#571,.T.);
#816=EDGE_CURVE('',#667,#668,#572,.T.);
#817=EDGE_CURVE('',#669,#668,#573,.T.);
#818=EDGE_CURVE('',#668,#669,#574,.T.);
#819=EDGE_CURVE('',#670,#670,#575,.T.);
#820=EDGE_CURVE('',#670,#671,#576,.T.);
#821=EDGE_CURVE('',#671,#671,#577,.T.);
#822=EDGE_CURVE('',#672,#673,#578,.T.);
#823=EDGE_CURVE('',#674,#672,#336,.T.);
#824=EDGE_CURVE('',#675,#674,#337,.T.);
#825=EDGE_CURVE('',#673,#675,#579,.T.);
#826=EDGE_CURVE('',#673,#676,#580,.T.);
#827=EDGE_CURVE('',#676,#676,#581,.T.);
#828=EDGE_CURVE('',#677,#677,#582,.T.);
#829=EDGE_CURVE('',#677,#678,#583,.T.);
#830=EDGE_CURVE('',#679,#678,#584,.T.);
#831=EDGE_CURVE('',#680,#679,#338,.T.);
#832=EDGE_CURVE('',#681,#680,#339,.T.);
#833=EDGE_CURVE('',#678,#681,#585,.T.);
#834=EDGE_CURVE('',#666,#675,#340,.F.);
#835=EDGE_CURVE('',#672,#665,#341,.T.);
#836=EDGE_CURVE('',#660,#681,#342,.F.);
#837=EDGE_CURVE('',#679,#659,#343,.T.);
#838=EDGE_CURVE('',#682,#683,#73,.T.);
#839=EDGE_CURVE('',#684,#682,#74,.T.);
#840=EDGE_CURVE('',#685,#684,#75,.T.);
#841=EDGE_CURVE('',#685,#670,#211,.T.);
#842=EDGE_CURVE('',#686,#685,#76,.T.);
#843=EDGE_CURVE('',#687,#686,#77,.T.);
#844=EDGE_CURVE('',#683,#687,#78,.T.);
#845=EDGE_CURVE('',#688,#689,#79,.T.);
#846=EDGE_CURVE('',#690,#688,#80,.T.);
#847=EDGE_CURVE('',#691,#690,#81,.T.);
#848=EDGE_CURVE('',#691,#669,#212,.T.);
#849=EDGE_CURVE('',#692,#691,#82,.T.);
#850=EDGE_CURVE('',#693,#692,#83,.T.);
#851=EDGE_CURVE('',#689,#693,#84,.T.);
#852=EDGE_CURVE('',#664,#662,#344,.T.);
#853=EDGE_CURVE('',#663,#661,#345,.F.);
#854=EDGE_CURVE('',#690,#682,#213,.T.);
#855=EDGE_CURVE('',#691,#683,#214,.T.);
#856=EDGE_CURVE('',#692,#687,#215,.T.);
#857=EDGE_CURVE('',#693,#686,#216,.T.);
#858=EDGE_CURVE('',#689,#685,#217,.T.);
#859=EDGE_CURVE('',#688,#684,#218,.T.);
#860=EDGE_CURVE('',#674,#680,#85,.T.);
#1081=ORIENTED_EDGE('',*,*,#804,.T.);
#1082=ORIENTED_EDGE('',*,*,#805,.T.);
#1083=ORIENTED_EDGE('',*,*,#806,.T.);
#1084=ORIENTED_EDGE('',*,*,#807,.F.);
#1085=ORIENTED_EDGE('',*,*,#808,.T.);
#1086=ORIENTED_EDGE('',*,*,#809,.T.);
#1087=ORIENTED_EDGE('',*,*,#804,.F.);
#1088=ORIENTED_EDGE('',*,*,#810,.F.);
#1089=ORIENTED_EDGE('',*,*,#811,.F.);
#1090=ORIENTED_EDGE('',*,*,#812,.F.);
#1091=ORIENTED_EDGE('',*,*,#813,.T.);
#1092=ORIENTED_EDGE('',*,*,#814,.T.);
#1093=ORIENTED_EDGE('',*,*,#815,.F.);
#1094=ORIENTED_EDGE('',*,*,#816,.T.);
#1095=ORIENTED_EDGE('',*,*,#817,.F.);
#1096=ORIENTED_EDGE('',*,*,#818,.F.);
#1097=ORIENTED_EDGE('',*,*,#816,.F.);
#1098=ORIENTED_EDGE('',*,*,#819,.F.);
#1099=ORIENTED_EDGE('',*,*,#820,.T.);
#1100=ORIENTED_EDGE('',*,*,#821,.F.);
#1101=ORIENTED_EDGE('',*,*,#820,.F.);
#1102=ORIENTED_EDGE('',*,*,#822,.F.);
#1103=ORIENTED_EDGE('',*,*,#823,.F.);
#1104=ORIENTED_EDGE('',*,*,#824,.F.);
#1105=ORIENTED_EDGE('',*,*,#825,.F.);
#1106=ORIENTED_EDGE('',*,*,#826,.T.);
#1107=ORIENTED_EDGE('',*,*,#827,.F.);
#1108=ORIENTED_EDGE('',*,*,#826,.F.);
#1109=ORIENTED_EDGE('',*,*,#828,.F.);
#1110=ORIENTED_EDGE('',*,*,#829,.T.);
#1111=ORIENTED_EDGE('',*,*,#830,.F.);
#1112=ORIENTED_EDGE('',*,*,#831,.F.);
#1113=ORIENTED_EDGE('',*,*,#832,.F.);
#1114=ORIENTED_EDGE('',*,*,#833,.F.);
#1115=ORIENTED_EDGE('',*,*,#829,.F.);
#1116=ORIENTED_EDGE('',*,*,#834,.F.);
#1117=ORIENTED_EDGE('',*,*,#813,.F.);
#1118=ORIENTED_EDGE('',*,*,#835,.F.);
#1119=ORIENTED_EDGE('',*,*,#822,.T.);
#1120=ORIENTED_EDGE('',*,*,#825,.T.);
#1121=ORIENTED_EDGE('',*,*,#836,.F.);
#1122=ORIENTED_EDGE('',*,*,#806,.F.);
#1123=ORIENTED_EDGE('',*,*,#837,.F.);
#1124=ORIENTED_EDGE('',*,*,#830,.T.);
#1125=ORIENTED_EDGE('',*,*,#833,.T.);
#1126=ORIENTED_EDGE('',*,*,#838,.F.);
#1127=ORIENTED_EDGE('',*,*,#839,.F.);
#1128=ORIENTED_EDGE('',*,*,#840,.F.);
#1129=ORIENTED_EDGE('',*,*,#841,.T.);
#1130=ORIENTED_EDGE('',*,*,#819,.T.);
#1131=ORIENTED_EDGE('',*,*,#841,.F.);
#1132=ORIENTED_EDGE('',*,*,#842,.F.);
#1133=ORIENTED_EDGE('',*,*,#843,.F.);
#1134=ORIENTED_EDGE('',*,*,#844,.F.);
#1135=ORIENTED_EDGE('',*,*,#845,.F.);
#1136=ORIENTED_EDGE('',*,*,#846,.F.);
#1137=ORIENTED_EDGE('',*,*,#847,.F.);
#1138=ORIENTED_EDGE('',*,*,#848,.T.);
#1139=ORIENTED_EDGE('',*,*,#817,.T.);
#1140=ORIENTED_EDGE('',*,*,#818,.T.);
#1141=ORIENTED_EDGE('',*,*,#848,.F.);
#1142=ORIENTED_EDGE('',*,*,#849,.F.);
#1143=ORIENTED_EDGE('',*,*,#850,.F.);
#1144=ORIENTED_EDGE('',*,*,#851,.F.);
#1145=ORIENTED_EDGE('',*,*,#811,.T.);
#1146=ORIENTED_EDGE('',*,*,#852,.T.);
#1147=ORIENTED_EDGE('',*,*,#808,.F.);
#1148=ORIENTED_EDGE('',*,*,#853,.F.);
#1149=ORIENTED_EDGE('',*,*,#815,.T.);
#1150=ORIENTED_EDGE('',*,*,#827,.T.);
#1151=ORIENTED_EDGE('',*,*,#821,.T.);
#1152=ORIENTED_EDGE('',*,*,#828,.T.);
#1153=ORIENTED_EDGE('',*,*,#854,.T.);
#1154=ORIENTED_EDGE('',*,*,#838,.T.);
#1155=ORIENTED_EDGE('',*,*,#855,.F.);
#1156=ORIENTED_EDGE('',*,*,#847,.T.);
#1157=ORIENTED_EDGE('',*,*,#855,.T.);
#1158=ORIENTED_EDGE('',*,*,#844,.T.);
#1159=ORIENTED_EDGE('',*,*,#856,.F.);
#1160=ORIENTED_EDGE('',*,*,#849,.T.);
#1161=ORIENTED_EDGE('',*,*,#856,.T.);
#1162=ORIENTED_EDGE('',*,*,#843,.T.);
#1163=ORIENTED_EDGE('',*,*,#857,.F.);
#1164=ORIENTED_EDGE('',*,*,#850,.T.);
#1165=ORIENTED_EDGE('',*,*,#857,.T.);
#1166=ORIENTED_EDGE('',*,*,#842,.T.);
#1167=ORIENTED_EDGE('',*,*,#858,.F.);
#1168=ORIENTED_EDGE('',*,*,#851,.T.);
#1169=ORIENTED_EDGE('',*,*,#858,.T.);
#1170=ORIENTED_EDGE('',*,*,#840,.T.);
#1171=ORIENTED_EDGE('',*,*,#859,.F.);
#1172=ORIENTED_EDGE('',*,*,#845,.T.);
#1173=ORIENTED_EDGE('',*,*,#859,.T.);
#1174=ORIENTED_EDGE('',*,*,#839,.T.);
#1175=ORIENTED_EDGE('',*,*,#854,.F.);
#1176=ORIENTED_EDGE('',*,*,#846,.T.);
#1177=ORIENTED_EDGE('',*,*,#836,.T.);
#1178=ORIENTED_EDGE('',*,*,#832,.T.);
#1179=ORIENTED_EDGE('',*,*,#860,.F.);
#1180=ORIENTED_EDGE('',*,*,#823,.T.);
#1181=ORIENTED_EDGE('',*,*,#835,.T.);
#1182=ORIENTED_EDGE('',*,*,#812,.T.);
#1183=ORIENTED_EDGE('',*,*,#853,.T.);
#1184=ORIENTED_EDGE('',*,*,#810,.T.);
#1185=ORIENTED_EDGE('',*,*,#807,.T.);
#1186=ORIENTED_EDGE('',*,*,#860,.T.);
#1187=ORIENTED_EDGE('',*,*,#831,.T.);
#1188=ORIENTED_EDGE('',*,*,#837,.T.);
#1189=ORIENTED_EDGE('',*,*,#805,.F.);
#1190=ORIENTED_EDGE('',*,*,#809,.F.);
#1191=ORIENTED_EDGE('',*,*,#852,.F.);
#1192=ORIENTED_EDGE('',*,*,#814,.F.);
#1193=ORIENTED_EDGE('',*,*,#834,.T.);
#1194=ORIENTED_EDGE('',*,*,#824,.T.);
#1200=TOROIDAL_SURFACE('',#1471,5.5021444402588,0.5);
#1201=TOROIDAL_SURFACE('',#1476,5.5021444402588,0.5);
#1202=TOROIDAL_SURFACE('',#1480,4.30710678118655,0.5);
#1203=TOROIDAL_SURFACE('',#1485,4.30710678118655,0.5);
#1258=ADVANCED_FACE('',(#400),#305,.F.);
#1259=ADVANCED_FACE('',(#401),#306,.F.);
#1260=ADVANCED_FACE('',(#402),#307,.F.);
#1261=ADVANCED_FACE('',(#403),#1200,.T.);
#1262=ADVANCED_FACE('',(#404),#1201,.T.);
#1263=ADVANCED_FACE('',(#405),#1202,.T.);
#1264=ADVANCED_FACE('',(#406),#1203,.T.);
#1265=ADVANCED_FACE('',(#407),#86,.F.);
#1266=ADVANCED_FACE('',(#408),#87,.F.);
#1267=ADVANCED_FACE('',(#409),#88,.T.);
#1268=ADVANCED_FACE('',(#410),#89,.T.);
#1269=ADVANCED_FACE('',(#411),#308,.F.);
#1270=ADVANCED_FACE('',(#412,#326),#144,.T.);
#1271=ADVANCED_FACE('',(#413,#327),#145,.F.);
#1272=ADVANCED_FACE('',(#414),#146,.F.);
#1273=ADVANCED_FACE('',(#415),#147,.F.);
#1274=ADVANCED_FACE('',(#416),#148,.F.);
#1275=ADVANCED_FACE('',(#417),#149,.F.);
#1276=ADVANCED_FACE('',(#418),#150,.F.);
#1277=ADVANCED_FACE('',(#419),#151,.F.);
#1278=ADVANCED_FACE('',(#420),#71,.F.);
#1279=ADVANCED_FACE('',(#421),#72,.F.);
#1285=CLOSED_SHELL('',(#1258,#1259,#1260,#1261,#1262,#1263,#1264,#1265,
#1266,#1267,#1268,#1269,#1270,#1271,#1272,#1273,#1274,#1275,#1276,#1277,
#1278,#1279));
#1465=AXIS2_PLACEMENT_3D('',#2200,#1798,#1799);
#1466=AXIS2_PLACEMENT_3D('',#2201,#1800,#1801);
#1467=AXIS2_PLACEMENT_3D('',#2243,#1803,#1804);
#1468=AXIS2_PLACEMENT_3D('',#2280,#1805,#1806);
#1469=AXIS2_PLACEMENT_3D('',#2356,#1808,#1809);
#1470=AXIS2_PLACEMENT_3D('',#2388,#1811,#1812);
#1471=AXIS2_PLACEMENT_3D('',#2415,#1813,#1814);
#1472=AXIS2_PLACEMENT_3D('',#2417,#1815,#1816);
#1473=AXIS2_PLACEMENT_3D('',#2419,#1817,#1818);
#1474=AXIS2_PLACEMENT_3D('',#2421,#1819,#1820);
#1475=AXIS2_PLACEMENT_3D('',#2422,#1821,#1822);
#1476=AXIS2_PLACEMENT_3D('',#2423,#1823,#1824);
#1477=AXIS2_PLACEMENT_3D('',#2425,#1825,#1826);
#1478=AXIS2_PLACEMENT_3D('',#2427,#1827,#1828);
#1479=AXIS2_PLACEMENT_3D('',#2428,#1829,#1830);
#1480=AXIS2_PLACEMENT_3D('',#2429,#1831,#1832);
#1481=AXIS2_PLACEMENT_3D('',#2432,#1833,#1834);
#1482=AXIS2_PLACEMENT_3D('',#2451,#1835,#1836);
#1483=AXIS2_PLACEMENT_3D('',#2453,#1837,#1838);
#1484=AXIS2_PLACEMENT_3D('',#2454,#1839,#1840);
#1485=AXIS2_PLACEMENT_3D('',#2455,#1841,#1842);
#1486=AXIS2_PLACEMENT_3D('',#2457,#1843,#1844);
#1487=AXIS2_PLACEMENT_3D('',#2459,#1845,#1846);
#1488=AXIS2_PLACEMENT_3D('',#2461,#1847,#1848);
#1489=AXIS2_PLACEMENT_3D('',#2480,#1849,#1850);
#1490=AXIS2_PLACEMENT_3D('',#2481,#1851,#1852);
#1491=AXIS2_PLACEMENT_3D('',#2527,#1853,#1854);
#1492=AXIS2_PLACEMENT_3D('',#2573,#1855,#1856);
#1493=AXIS2_PLACEMENT_3D('',#2599,#1858,#1859);
#1494=AXIS2_PLACEMENT_3D('',#2625,#1861,#1862);
#1495=AXIS2_PLACEMENT_3D('',#2698,#1863,#1864);
#1496=AXIS2_PLACEMENT_3D('',#2699,#1865,#1866);
#1497=AXIS2_PLACEMENT_3D('',#2700,#1867,#1868);
#1498=AXIS2_PLACEMENT_3D('',#2703,#1871,#1872);
#1499=AXIS2_PLACEMENT_3D('',#2705,#1874,#1875);
#1500=AXIS2_PLACEMENT_3D('',#2707,#1877,#1878);
#1501=AXIS2_PLACEMENT_3D('',#2709,#1880,#1881);
#1502=AXIS2_PLACEMENT_3D('',#2711,#1883,#1884);
#1798=DIRECTION('axis',(0.,0.,1.));
#1799=DIRECTION('refdir',(1.,0.,0.));
#1800=DIRECTION('center_axis',(0.,0.,-1.));
#1801=DIRECTION('ref_axis',(-1.,0.,0.));
#1802=DIRECTION('',(0.,0.,-1.));
#1803=DIRECTION('center_axis',(0.,0.,-1.));
#1804=DIRECTION('ref_axis',(1.,-2.1316282072803E-14,0.));
#1805=DIRECTION('center_axis',(0.,0.,-1.));
#1806=DIRECTION('ref_axis',(-1.,0.,0.));
#1807=DIRECTION('',(0.,0.,-1.));
#1808=DIRECTION('center_axis',(0.,0.,-1.));
#1809=DIRECTION('ref_axis',(-1.,0.,0.));
#1810=DIRECTION('',(0.,0.,-1.));
#1811=DIRECTION('center_axis',(0.,0.,1.));
#1812=DIRECTION('ref_axis',(1.,0.,0.));
#1813=DIRECTION('center_axis',(0.,0.,1.));
#1814=DIRECTION('ref_axis',(1.,0.,0.));
#1815=DIRECTION('center_axis',(0.,0.,1.));
#1816=DIRECTION('ref_axis',(1.,0.,0.));
#1817=DIRECTION('center_axis',(1.22464679914735E-16,-1.,0.));
#1818=DIRECTION('ref_axis',(-1.,-1.22464679914735E-16,0.));
#1819=DIRECTION('center_axis',(0.,0.,-1.));
#1820=DIRECTION('ref_axis',(-1.,0.,0.));
#1821=DIRECTION('center_axis',(0.,0.,-1.));
#1822=DIRECTION('ref_axis',(-1.,0.,0.));
#1823=DIRECTION('center_axis',(0.,0.,1.));
#1824=DIRECTION('ref_axis',(1.,0.,0.));
#1825=DIRECTION('center_axis',(0.,0.,1.));
#1826=DIRECTION('ref_axis',(-1.,0.,0.));
#1827=DIRECTION('center_axis',(1.22464679914735E-16,-1.,0.));
#1828=DIRECTION('ref_axis',(-1.,-1.22464679914735E-16,0.));
#1829=DIRECTION('center_axis',(0.,0.,-1.));
#1830=DIRECTION('ref_axis',(1.,0.,0.));
#1831=DIRECTION('center_axis',(0.,0.,1.));
#1832=DIRECTION('ref_axis',(1.,0.,0.));
#1833=DIRECTION('center_axis',(0.,0.,1.));
#1834=DIRECTION('ref_axis',(-1.,0.,0.));
#1835=DIRECTION('center_axis',(0.,0.,1.));
#1836=DIRECTION('ref_axis',(-1.,0.,0.));
#1837=DIRECTION('center_axis',(1.22464679914735E-16,-1.,0.));
#1838=DIRECTION('ref_axis',(-1.,-1.22464679914735E-16,0.));
#1839=DIRECTION('center_axis',(0.,0.,-1.));
#1840=DIRECTION('ref_axis',(1.,0.,0.));
#1841=DIRECTION('center_axis',(0.,0.,1.));
#1842=DIRECTION('ref_axis',(1.,0.,0.));
#1843=DIRECTION('center_axis',(0.,0.,1.));
#1844=DIRECTION('ref_axis',(1.,0.,0.));
#1845=DIRECTION('center_axis',(1.22464679914735E-16,-1.,0.));
#1846=DIRECTION('ref_axis',(-1.,-1.22464679914735E-16,0.));
#1847=DIRECTION('center_axis',(0.,0.,-1.));
#1848=DIRECTION('ref_axis',(-1.,0.,0.));
#1849=DIRECTION('center_axis',(0.,0.,-1.));
#1850=DIRECTION('ref_axis',(-1.,0.,0.));
#1851=DIRECTION('center_axis',(0.,0.,1.));
#1852=DIRECTION('ref_axis',(0.653358928956991,0.757048287728183,0.));
#1853=DIRECTION('center_axis',(0.,0.,-1.));
#1854=DIRECTION('ref_axis',(-0.901632299434182,-0.432503406480261,0.));
#1855=DIRECTION('center_axis',(0.,0.,1.));
#1856=DIRECTION('ref_axis',(1.,0.,0.));
#1857=DIRECTION('',(0.880471099922175,1.07826611426144E-16,-0.474099823035018));
#1858=DIRECTION('center_axis',(0.,0.,-1.));
#1859=DIRECTION('ref_axis',(-1.,0.,0.));
#1860=DIRECTION('',(-0.880471099922175,1.07826611426144E-16,0.474099823035018));
#1861=DIRECTION('center_axis',(0.,0.,-1.));
#1862=DIRECTION('ref_axis',(-1.,0.,0.));
#1863=DIRECTION('center_axis',(0.,0.,1.));
#1864=DIRECTION('ref_axis',(1.,0.,0.));
#1865=DIRECTION('center_axis',(0.,0.,1.));
#1866=DIRECTION('ref_axis',(1.,0.,0.));
#1867=DIRECTION('center_axis',(-0.866025403784438,0.500000000000001,0.));
#1868=DIRECTION('ref_axis',(-0.500000000000001,-0.866025403784438,0.));
#1869=DIRECTION('',(0.,0.,-1.));
#1870=DIRECTION('',(0.,0.,-1.));
#1871=DIRECTION('center_axis',(-0.866025403784439,-0.499999999999999,0.));
#1872=DIRECTION('ref_axis',(0.499999999999999,-0.866025403784439,0.));
#1873=DIRECTION('',(0.,0.,-1.));
#1874=DIRECTION('center_axis',(0.,-1.,0.));
#1875=DIRECTION('ref_axis',(0.,0.,-1.));
#1876=DIRECTION('',(0.,0.,-1.));
#1877=DIRECTION('center_axis',(0.866025403784439,-0.5,0.));
#1878=DIRECTION('ref_axis',(0.5,0.866025403784439,0.));
#1879=DIRECTION('',(0.,0.,-1.));
#1880=DIRECTION('center_axis',(0.866025403784438,0.500000000000001,0.));
#1881=DIRECTION('ref_axis',(-0.500000000000001,0.866025403784438,0.));
#1882=DIRECTION('',(0.,0.,-1.));
#1883=DIRECTION('center_axis',(-1.00154306582477E-15,1.,0.));
#1884=DIRECTION('ref_axis',(-1.,-1.00154306582477E-15,0.));
#2200=CARTESIAN_POINT('',(0.,0.,0.));
#2201=CARTESIAN_POINT('Origin',(0.,0.,6.));
#2202=CARTESIAN_POINT('',(3.4,1.886685021085E-13,1.93750000000002));
#2203=CARTESIAN_POINT('',(3.4,-1.7333563370988E-13,1.92749999999998));
#2204=CARTESIAN_POINT('',(3.4,-4.163799117101E-16,6.));
#2205=CARTESIAN_POINT('',(3.37685862035149,0.396012446973337,0.700000000000002));
#2206=CARTESIAN_POINT('Ctrl Pts',(3.4,-3.4625488750805E-13,1.92749999999998));
#2207=CARTESIAN_POINT('Ctrl Pts',(3.39999999999999,-0.0751214124647497,
1.92333274051478));
#2208=CARTESIAN_POINT('Ctrl Pts',(3.39751039970816,-0.150316128865589,1.91910420870307));
#2209=CARTESIAN_POINT('Ctrl Pts',(3.36253534799724,-0.676583934114712,1.88910655418598));
#2210=CARTESIAN_POINT('Ctrl Pts',(3.24287468221216,-1.11718618023821,1.86191518047301));
#2211=CARTESIAN_POINT('Ctrl Pts',(2.84552536189263,-1.91128615387662,1.80873328142527));
#2212=CARTESIAN_POINT('Ctrl Pts',(2.57731571088716,-2.25995921897011,1.78416891830816));
#2213=CARTESIAN_POINT('Ctrl Pts',(1.91158513943287,-2.84788181098038,1.73372915804847));
#2214=CARTESIAN_POINT('Ctrl Pts',(1.51622136776119,-3.07661995617186,1.70654095205508));
#2215=CARTESIAN_POINT('Ctrl Pts',(0.674677953708942,-3.36078822430551,1.65332785941573));
#2216=CARTESIAN_POINT('Ctrl Pts',(0.238650846294366,-3.41951310237242,1.62868720616195));
#2217=CARTESIAN_POINT('Ctrl Pts',(-0.648283414878094,-3.36815779516296,
1.5783056797496));
#2218=CARTESIAN_POINT('Ctrl Pts',(-1.09025108249999,-3.25208205777719,1.55112093538634));
#2219=CARTESIAN_POINT('Ctrl Pts',(-1.88804380928579,-2.86102085156782,1.49787867373243));
#2220=CARTESIAN_POINT('Ctrl Pts',(-2.23899450631159,-2.59556991721883,1.47316327182734));
#2221=CARTESIAN_POINT('Ctrl Pts',(-2.8325994386573,-1.93424395427837,1.42283728282858));
#2222=CARTESIAN_POINT('Ctrl Pts',(-3.06464870302035,-1.54038056751001,1.39565622597147));
#2223=CARTESIAN_POINT('Ctrl Pts',(-3.35550133962885,-0.700588956999663,
1.34238671925571));
#2224=CARTESIAN_POINT('Ctrl Pts',(-3.41759775458745,-0.264883297406569,
1.31759840541435));
#2225=CARTESIAN_POINT('Ctrl Pts',(-3.37299216600685,0.622892781759607,1.26732527491678));
#2226=CARTESIAN_POINT('Ctrl Pts',(-3.26013973203468,1.06605967034742,1.24014807025696));
#2227=CARTESIAN_POINT('Ctrl Pts',(-2.87472803373432,1.86714190123431,1.18685314184052));
#2228=CARTESIAN_POINT('Ctrl Pts',(-2.61174512528069,2.2201316660374,1.16199399900912));
#2229=CARTESIAN_POINT('Ctrl Pts',(-1.95437463831632,2.81880032541014,1.11177108070705));
#2230=CARTESIAN_POINT('Ctrl Pts',(-1.56187370908267,3.05379875999433,1.08459783849235));
#2231=CARTESIAN_POINT('Ctrl Pts',(-0.723668687168632,3.35061944763769,1.03127921212292));
#2232=CARTESIAN_POINT('Ctrl Pts',(-0.288248857360501,3.415723993581,1.00635152330788));
#2233=CARTESIAN_POINT('Ctrl Pts',(0.600256135722737,3.37713545522293,0.956176216715607));
#2234=CARTESIAN_POINT('Ctrl Pts',(1.04447166788701,3.26716227445194,0.929006999272162));
#2235=CARTESIAN_POINT('Ctrl Pts',(1.84846805982719,2.88679407269544,0.875666300851262));
#2236=CARTESIAN_POINT('Ctrl Pts',(2.20327250640915,2.62600628040714,0.850672506218438));
#2237=CARTESIAN_POINT('Ctrl Pts',(2.74028398997315,2.04386855383655,0.806039779237286));
#2238=CARTESIAN_POINT('Ctrl Pts',(2.93894310375689,1.74617193811401,0.784960681789362));
#2239=CARTESIAN_POINT('Ctrl Pts',(3.23761590955786,1.0981423198909,0.742149222714576));
#2240=CARTESIAN_POINT('Ctrl Pts',(3.33517029647866,0.751495151908227,0.720677837576191));
#2241=CARTESIAN_POINT('Ctrl Pts',(3.37685862035149,0.396012446973369,0.700000000000005));
#2242=CARTESIAN_POINT('',(3.39272377138046,0.222318265353878,0.700000000000003));
#2243=CARTESIAN_POINT('Origin',(0.,0.,0.700000000000003));
#2244=CARTESIAN_POINT('Ctrl Pts',(3.39272377138046,0.222318265353877,0.700000000000002));
#2245=CARTESIAN_POINT('Ctrl Pts',(3.37412547491926,0.506140570330221,0.716172011820753));
#2246=CARTESIAN_POINT('Ctrl Pts',(3.31998703241798,0.786485391117649,0.732967754260724));
#2247=CARTESIAN_POINT('Ctrl Pts',(3.14234381547146,1.32971112277357,0.767184347683065));
#2248=CARTESIAN_POINT('Ctrl Pts',(3.01887224077644,1.59024336880604,0.784474146775485));
#2249=CARTESIAN_POINT('Ctrl Pts',(2.62760958855879,2.20188958075105,0.827394809286271));
#2250=CARTESIAN_POINT('Ctrl Pts',(2.32175071403847,2.5223253300443,0.851036839792356));
#2251=CARTESIAN_POINT('Ctrl Pts',(1.5999770548258,3.03286055950024,0.902807312827531));
#2252=CARTESIAN_POINT('Ctrl Pts',(1.18957513867269,3.21606383785568,0.929783442201523));
#2253=CARTESIAN_POINT('Ctrl Pts',(0.327205679871517,3.41261700251858,0.982138617014873));
#2254=CARTESIAN_POINT('Ctrl Pts',(-0.115991804276865,3.42630500609258,1.00583005470857));
#2255=CARTESIAN_POINT('Ctrl Pts',(-0.988539108930611,3.28339257492864,1.05751727823502));
#2256=CARTESIAN_POINT('Ctrl Pts',(-1.4091646726289,3.12603795168328,1.0844666018519));
#2257=CARTESIAN_POINT('Ctrl Pts',(-2.16163383983647,2.6609667424342,1.13689519739393));
#2258=CARTESIAN_POINT('Ctrl Pts',(-2.48730708019587,2.35938761807513,1.16064433579374));
#2259=CARTESIAN_POINT('Ctrl Pts',(-3.00855100939004,1.64505569074969,1.21224805261772));
#2260=CARTESIAN_POINT('Ctrl Pts',(-3.19761651264121,1.23806873692515,1.23916944340088));
#2261=CARTESIAN_POINT('Ctrl Pts',(-3.4074155924874,0.378584884973299,1.2916689069089));
#2262=CARTESIAN_POINT('Ctrl Pts',(-3.42776120331645,-0.0652819333619287,
1.31548353229742));
#2263=CARTESIAN_POINT('Ctrl Pts',(-3.29751165500039,-0.94006407528417,1.36700376344325));
#2264=CARTESIAN_POINT('Ctrl Pts',(-3.14663149078755,-1.36234659974212,1.39389623499455));
#2265=CARTESIAN_POINT('Ctrl Pts',(-2.69283660283573,-2.12199326490917,1.44646388595065));
#2266=CARTESIAN_POINT('Ctrl Pts',(-2.3954353691001,-2.45277677318083,1.4703511998463));
#2267=CARTESIAN_POINT('Ctrl Pts',(-1.68838832626413,-2.98435427657513,1.52178824174531));
#2268=CARTESIAN_POINT('Ctrl Pts',(-1.28478836071299,-3.17904312972706,1.54865095690521));
#2269=CARTESIAN_POINT('Ctrl Pts',(-0.428205698086118,-3.40166035571351,
1.60128401543907));
#2270=CARTESIAN_POINT('Ctrl Pts',(0.0163083473326349,-3.42846701123013,
1.6252505703603));
#2271=CARTESIAN_POINT('Ctrl Pts',(0.893164120516335,-3.31043983444755,1.6766049884818));
#2272=CARTESIAN_POINT('Ctrl Pts',(1.31695104779562,-3.16581130059277,1.70343726516491));
#2273=CARTESIAN_POINT('Ctrl Pts',(2.08342989700817,-2.72294177772439,1.75613287996062));
#2274=CARTESIAN_POINT('Ctrl Pts',(2.41914338179383,-2.42957489515017,1.78018452939157));
#2275=CARTESIAN_POINT('Ctrl Pts',(2.96058323228635,-1.72957694899934,1.83145714854881));
#2276=CARTESIAN_POINT('Ctrl Pts',(3.16060634091826,-1.32929335181225,1.85825846283549));
#2277=CARTESIAN_POINT('Ctrl Pts',(3.35919394319754,-0.607510420852717,1.90286153598097));
#2278=CARTESIAN_POINT('Ctrl Pts',(3.4,-0.304158067979466,1.92062723959507));
#2279=CARTESIAN_POINT('Ctrl Pts',(3.4,3.75914577244174E-13,1.93750000000002));
#2280=CARTESIAN_POINT('Origin',(0.,0.,6.));
#2281=CARTESIAN_POINT('',(3.4,2.00975518948028E-13,3.18750000000002));
#2282=CARTESIAN_POINT('',(3.4,-2.31845815703038E-13,3.17749999999997));
#2283=CARTESIAN_POINT('',(3.4,-4.163799117101E-16,6.));
#2284=CARTESIAN_POINT('Ctrl Pts',(3.4,-4.60083360298569E-13,3.17749999999997));
#2285=CARTESIAN_POINT('Ctrl Pts',(3.39999999999998,-0.124055612801236,3.17061818145879));
#2286=CARTESIAN_POINT('Ctrl Pts',(3.39321082219142,-0.248246409564226,3.16357286244051));
#2287=CARTESIAN_POINT('Ctrl Pts',(3.33116756101355,-0.811870855624036,3.13088092671118));
#2288=CARTESIAN_POINT('Ctrl Pts',(3.19734659839163,-1.23803930410971,3.10416487407304));
#2289=CARTESIAN_POINT('Ctrl Pts',(2.77346040786446,-2.01610650879456,3.05126260871194));
#2290=CARTESIAN_POINT('Ctrl Pts',(2.48707839500391,-2.36033777798621,3.02685663175361));
#2291=CARTESIAN_POINT('Ctrl Pts',(1.7929353991586,-2.92374484925883,2.97540404659579));
#2292=CARTESIAN_POINT('Ctrl Pts',(1.39026664782006,-3.1352848688268,2.94820578418326));
#2293=CARTESIAN_POINT('Ctrl Pts',(0.54010689947229,-3.3849815708294,2.8953067975875));
#2294=CARTESIAN_POINT('Ctrl Pts',(0.102397368140257,-3.42626792230477,2.87128393927437));
#2295=CARTESIAN_POINT('Ctrl Pts',(-0.779759552893679,-3.3399279964116,2.82036355488111));
#2296=CARTESIAN_POINT('Ctrl Pts',(-1.21512493198708,-3.20726728549062,2.79316397506227));
#2297=CARTESIAN_POINT('Ctrl Pts',(-1.99552112635261,-2.7870613886808,2.74021707769849));
#2298=CARTESIAN_POINT('Ctrl Pts',(-2.33583968220507,-2.50871391944311,2.71611974922401));
#2299=CARTESIAN_POINT('Ctrl Pts',(-2.90268788574612,-1.82695946513531,2.66527533163809));
#2300=CARTESIAN_POINT('Ctrl Pts',(-3.11913619711619,-1.4262931678841,2.6380753702369));
#2301=CARTESIAN_POINT('Ctrl Pts',(-3.3786317075168,-0.578512038455339,2.58508317788875));
#2302=CARTESIAN_POINT('Ctrl Pts',(-3.42488520840102,-0.141285215142229,
2.56090941845037));
#2303=CARTESIAN_POINT('Ctrl Pts',(-3.34851993642526,0.74230513788558,2.51013871335301));
#2304=CARTESIAN_POINT('Ctrl Pts',(-3.22056580886756,1.17961881649017,2.48293920183057));
#2305=CARTESIAN_POINT('Ctrl Pts',(-2.80864605558055,1.96503421009277,2.42990426964723));
#2306=CARTESIAN_POINT('Ctrl Pts',(-2.53399448601039,2.30839566056453,2.40565276182308));
#2307=CARTESIAN_POINT('Ctrl Pts',(-1.8580511213592,2.8829610420091,2.35495338177295));
#2308=CARTESIAN_POINT('Ctrl Pts',(-1.45927879698983,3.10391090200561,2.32775504965466));
#2309=CARTESIAN_POINT('Ctrl Pts',(-0.613734967667859,3.37241972842292,2.2746798610805));
#2310=CARTESIAN_POINT('Ctrl Pts',(-0.176948946422862,3.42323463003873,2.25034988916224));
#2311=CARTESIAN_POINT('Ctrl Pts',(0.707906623729064,3.35602338427,2.19971933851952));
#2312=CARTESIAN_POINT('Ctrl Pts',(1.14696212981517,3.23240453137218,2.17252281714256));
#2313=CARTESIAN_POINT('Ctrl Pts',(1.93694225593166,2.82810566485756,2.11940977484039));
#2314=CARTESIAN_POINT('Ctrl Pts',(2.28308793287607,2.55683229388904,2.09500117802721));
#2315=CARTESIAN_POINT('Ctrl Pts',(2.86467311712893,1.88623164311572,2.04443687723939));
#2316=CARTESIAN_POINT('Ctrl Pts',(3.08971677030665,1.48923000405015,2.01724270457179));
#2317=CARTESIAN_POINT('Ctrl Pts',(3.34296531938119,0.717336589060177,1.96860382359178));
#2318=CARTESIAN_POINT('Ctrl Pts',(3.40000000000004,0.359580275069644,1.9474472329236));
#2319=CARTESIAN_POINT('Ctrl Pts',(3.4,-3.45973250048814E-13,1.92749999999998));
#2320=CARTESIAN_POINT('Ctrl Pts',(3.4,3.74526798463393E-13,1.93750000000002));
#2321=CARTESIAN_POINT('Ctrl Pts',(3.4,0.136279469776807,1.94505992059303));
#2322=CARTESIAN_POINT('Ctrl Pts',(3.39180705844705,0.272699724057435,1.95281590794641));
#2323=CARTESIAN_POINT('Ctrl Pts',(3.3221402026329,0.84830236752116,1.98634749260179));
#2324=CARTESIAN_POINT('Ctrl Pts',(3.18348028608021,1.2734386993689,2.01311747915411));
#2325=CARTESIAN_POINT('Ctrl Pts',(2.75107870203134,2.04635190683021,2.06592949965133));
#2326=CARTESIAN_POINT('Ctrl Pts',(2.46156686998329,2.38676981770287,2.09016593969441));
#2327=CARTESIAN_POINT('Ctrl Pts',(1.7683141254283,2.93752419790701,2.14127840656622));
#2328=CARTESIAN_POINT('Ctrl Pts',(1.37123772364491,3.14255430517566,2.16801685651457));
#2329=CARTESIAN_POINT('Ctrl Pts',(0.520350566691976,3.3890530057568,2.22088271163742));
#2330=CARTESIAN_POINT('Ctrl Pts',(0.074636608528427,3.42795309007607,2.24521732990269));
#2331=CARTESIAN_POINT('Ctrl Pts',(-0.80585263247956,3.33261816792688,2.29625188848068));
#2332=CARTESIAN_POINT('Ctrl Pts',(-1.23218612599118,3.19959587461778,2.32295874499352));
#2333=CARTESIAN_POINT('Ctrl Pts',(-2.01109866267633,2.77711773964354,2.37587554979457));
#2334=CARTESIAN_POINT('Ctrl Pts',(-2.35595932548207,2.49125279947127,2.40031119093976));
#2335=CARTESIAN_POINT('Ctrl Pts',(-2.91542455075476,1.80438620286028,2.45126955211513));
#2336=CARTESIAN_POINT('Ctrl Pts',(-3.12510855551194,1.41037495197566,2.47794490391592));
#2337=CARTESIAN_POINT('Ctrl Pts',(-3.38249509927501,0.562211989160962,2.5309098182471));
#2338=CARTESIAN_POINT('Ctrl Pts',(-3.42693586011265,0.115955599795384,2.55544858819458));
#2339=CARTESIAN_POINT('Ctrl Pts',(-3.34191394517752,-0.766092246809965,
2.60633263665211));
#2340=CARTESIAN_POINT('Ctrl Pts',(-3.21416329916218,-1.19347755885311,2.63297670978421));
#2341=CARTESIAN_POINT('Ctrl Pts',(-2.80099829533727,-1.9779321294727,2.68598695489635));
#2342=CARTESIAN_POINT('Ctrl Pts',(-2.51855061492812,-2.32694748215833,2.71063024885284));
#2343=CARTESIAN_POINT('Ctrl Pts',(-1.83766994494307,-2.89448448470946,2.76144202160989));
#2344=CARTESIAN_POINT('Ctrl Pts',(-1.44655561860144,-3.10845518160647,2.78805516977141));
#2345=CARTESIAN_POINT('Ctrl Pts',(-0.600995270357083,-3.37595293922109,
2.84110804243113));
#2346=CARTESIAN_POINT('Ctrl Pts',(-0.15423889345412,-3.42555594121709,2.86585658157997));
#2347=CARTESIAN_POINT('Ctrl Pts',(0.738999393540461,-3.349257097536,2.91716096647369));
#2348=CARTESIAN_POINT('Ctrl Pts',(1.17648243519229,-3.22171906800927,2.94436031210768));
#2349=CARTESIAN_POINT('Ctrl Pts',(1.96233836056712,-2.81053122123338,2.99740286449479));
#2350=CARTESIAN_POINT('Ctrl Pts',(2.30596779573501,-2.53620495219765,3.02166882819812));
#2351=CARTESIAN_POINT('Ctrl Pts',(2.88121057228278,-1.86077478462052,3.0723553044745));
#2352=CARTESIAN_POINT('Ctrl Pts',(3.1025555253124,-1.4621713365509,3.09955334683131));
#2353=CARTESIAN_POINT('Ctrl Pts',(3.34604860374013,-0.697838904257899,3.14754863181823));
#2354=CARTESIAN_POINT('Ctrl Pts',(3.4,-0.349728288913788,3.16809929277934));
#2355=CARTESIAN_POINT('Ctrl Pts',(3.4,4.01761957036229E-13,3.18750000000002));
#2356=CARTESIAN_POINT('Origin',(0.,0.,6.));
#2357=CARTESIAN_POINT('',(3.4,6.57668130322999E-14,4.43750000000001));
#2358=CARTESIAN_POINT('',(3.4,-2.15973304146491E-14,4.4275));
#2359=CARTESIAN_POINT('',(3.4,-4.163799117101E-16,6.));
#2360=CARTESIAN_POINT('',(-1.25288796387014,-3.16073911450935,5.3));
#2361=CARTESIAN_POINT('Ctrl Pts',(3.4,1.3195000597631E-13,4.43750000000001));
#2362=CARTESIAN_POINT('Ctrl Pts',(3.4,0.0484846749858157,4.44018962224077));
#2363=CARTESIAN_POINT('Ctrl Pts',(3.39896290803393,0.0970055128088234,4.44290508080457));
#2364=CARTESIAN_POINT('Ctrl Pts',(3.37748646850743,0.598298156849321,4.47120710147293));
#2365=CARTESIAN_POINT('Ctrl Pts',(3.26776257798046,1.04260348636478,4.49837557212729));
#2366=CARTESIAN_POINT('Ctrl Pts',(2.88783093020024,1.84685112659429,4.55172017709808));
#2367=CARTESIAN_POINT('Ctrl Pts',(2.62723278700067,2.20181240090978,4.57672590475695));
#2368=CARTESIAN_POINT('Ctrl Pts',(1.97369731242403,2.80535577064492,4.62684809170433));
#2369=CARTESIAN_POINT('Ctrl Pts',(1.58253065942841,3.04319173163336,4.65401251725117));
#2370=CARTESIAN_POINT('Ctrl Pts',(0.745875918244429,3.34576782876138,4.70737739133936));
#2371=CARTESIAN_POINT('Ctrl Pts',(0.310730749827996,3.41377166583742,4.7324461843677));
#2372=CARTESIAN_POINT('Ctrl Pts',(-0.578457082509039,3.38097745401162,4.78252622885647));
#2373=CARTESIAN_POINT('Ctrl Pts',(-1.02366424672491,3.27378194584287,4.80968663055877));
#2374=CARTESIAN_POINT('Ctrl Pts',(-1.83045062995484,2.89827699340989,4.86307035254325));
#2375=CARTESIAN_POINT('Ctrl Pts',(-2.18699995734974,2.63959876703994,4.88819955916222));
#2376=CARTESIAN_POINT('Ctrl Pts',(-2.79445461069521,1.98915973325728,4.9382398484591));
#2377=CARTESIAN_POINT('Ctrl Pts',(-3.03456603866918,1.5990797670419,4.96539627706253));
#2378=CARTESIAN_POINT('Ctrl Pts',(-3.34176724206059,0.763685305137532,5.01879751426961));
#2379=CARTESIAN_POINT('Ctrl Pts',(-3.41209993472139,0.328760199170906,5.04398443781417));
#2380=CARTESIAN_POINT('Ctrl Pts',(-3.38395618451195,-0.560962172903048,
5.09398727714361));
#2381=CARTESIAN_POINT('Ctrl Pts',(-3.27899342481953,-1.00695228698157,5.12113980797507));
#2382=CARTESIAN_POINT('Ctrl Pts',(-2.90739622987095,-1.81596630216988,5.17455731262962));
#2383=CARTESIAN_POINT('Ctrl Pts',(-2.65040817232962,-2.17391423643435,5.19979923899294));
#2384=CARTESIAN_POINT('Ctrl Pts',(-2.01958836457687,-2.76887523380191,5.24846409957791));
#2385=CARTESIAN_POINT('Ctrl Pts',(-1.65308929437083,-3.00210298164807,5.27415423684201));
#2386=CARTESIAN_POINT('Ctrl Pts',(-1.25288796387014,-3.16073911450935,5.3));
#2387=CARTESIAN_POINT('',(-1.0964822158325,-3.21834223636379,5.3));
#2388=CARTESIAN_POINT('Origin',(0.,0.,5.3));
#2389=CARTESIAN_POINT('Ctrl Pts',(-1.0964822158325,-3.21834223636379,5.3));
#2390=CARTESIAN_POINT('Ctrl Pts',(-1.45430969353474,-3.09643119122895,5.27734873633288));
#2391=CARTESIAN_POINT('Ctrl Pts',(-1.78932501450223,-2.9156906147822,5.25461116491904));
#2392=CARTESIAN_POINT('Ctrl Pts',(-2.38035325487317,-2.45588612176912,5.21125930631007));
#2393=CARTESIAN_POINT('Ctrl Pts',(-2.63375551357983,-2.18192473180001,5.1911460653954));
#2394=CARTESIAN_POINT('Ctrl Pts',(-3.08389885895375,-1.49967564665538,5.14295584619396));
#2395=CARTESIAN_POINT('Ctrl Pts',(-3.25401415229429,-1.08206016471883,5.11588028889413));
#2396=CARTESIAN_POINT('Ctrl Pts',(-3.42138906401064,-0.213729663558886,
5.06386488944011));
#2397=CARTESIAN_POINT('Ctrl Pts',(-3.4204678818224,0.227997362699221,5.04032246223822));
#2398=CARTESIAN_POINT('Ctrl Pts',(-3.24953923825127,1.0952858313522,4.9882832106968));
#2399=CARTESIAN_POINT('Ctrl Pts',(-3.07788020472564,1.51188914513325,4.96122833009511));
#2400=CARTESIAN_POINT('Ctrl Pts',(-2.58801584204305,2.24812277445386,4.90913068359549));
#2401=CARTESIAN_POINT('Ctrl Pts',(-2.27718857434759,2.56247822644399,4.88556850445372));
#2402=CARTESIAN_POINT('Ctrl Pts',(-1.54680891679612,3.06043075287894,4.83360974982649));
#2403=CARTESIAN_POINT('Ctrl Pts',(-1.1325180731347,3.23670388222288,4.80657712797727));
#2404=CARTESIAN_POINT('Ctrl Pts',(-0.266912011122178,3.41774214395029,4.75439890747381));
#2405=CARTESIAN_POINT('Ctrl Pts',(0.175502624023416,3.42365349401457,4.73080773618714));
#2406=CARTESIAN_POINT('Ctrl Pts',(1.04531165999775,3.26586547764908,4.67893060411707));
#2407=CARTESIAN_POINT('Ctrl Pts',(1.46386269391496,3.10091128189926,4.65192173972419));
#2408=CARTESIAN_POINT('Ctrl Pts',(2.20777213360059,2.62264912216571,4.59966488268835));
#2409=CARTESIAN_POINT('Ctrl Pts',(2.52743823870374,2.31616140221252,4.57603561652486));
#2410=CARTESIAN_POINT('Ctrl Pts',(3.03638972506586,1.59329637088458,4.52424099224271));
#2411=CARTESIAN_POINT('Ctrl Pts',(3.21872315951981,1.18239761726984,4.49725728869968));
#2412=CARTESIAN_POINT('Ctrl Pts',(3.37218516276219,0.501993715429373,4.45598655499202));
#2413=CARTESIAN_POINT('Ctrl Pts',(3.4,0.251114956290832,4.44143026500901));
#2414=CARTESIAN_POINT('Ctrl Pts',(3.4,-4.10088629720917E-14,4.4275));
#2415=CARTESIAN_POINT('Origin',(0.,0.,5.5));
#2416=CARTESIAN_POINT('',(-5.5021444402588,-6.73818357720935E-16,6.));
#2417=CARTESIAN_POINT('Origin',(0.,0.,6.));
#2418=CARTESIAN_POINT('',(-5.73919435177631,-7.02848599258743E-16,5.94023554996109));
#2419=CARTESIAN_POINT('Origin',(-5.5021444402588,-6.73818357720935E-16,
5.5));
#2420=CARTESIAN_POINT('',(5.73919435177631,7.76091229894499E-16,5.94023554996109));
#2421=CARTESIAN_POINT('Origin',(0.,0.,5.94023554996109));
#2422=CARTESIAN_POINT('Origin',(0.,0.,5.94023554996109));
#2423=CARTESIAN_POINT('Origin',(0.,0.,0.5));
#2424=CARTESIAN_POINT('',(-5.73919435177631,-7.02848599258743E-16,0.0597644500389123));
#2425=CARTESIAN_POINT('Origin',(0.,0.,0.0597644500389123));
#2426=CARTESIAN_POINT('',(-5.5021444402588,-6.73818357720935E-16,0.));
#2427=CARTESIAN_POINT('Origin',(-5.5021444402588,-6.73818357720935E-16,
0.5));
#2428=CARTESIAN_POINT('Origin',(0.,0.,0.));
#2429=CARTESIAN_POINT('Origin',(0.,0.,5.5));
#2430=CARTESIAN_POINT('',(-1.78291230217383,-3.52871196543851,5.8535533905933));
#2431=CARTESIAN_POINT('',(-3.95355339059327,-4.84170650504822E-16,5.85355339059327));
#2432=CARTESIAN_POINT('Origin',(0.,0.,5.85355339059327));
#2433=CARTESIAN_POINT('',(-1.92533487773279,-3.50614968428127,5.89456992403025));
#2434=CARTESIAN_POINT('Ctrl Pts',(-1.92533487773279,-3.50614968428128,5.89456992403026));
#2435=CARTESIAN_POINT('Ctrl Pts',(-1.90194360167476,-3.5135341387333,5.89084462065203));
#2436=CARTESIAN_POINT('Ctrl Pts',(-1.87630613215172,-3.52080459320752,5.88625665441102));
#2437=CARTESIAN_POINT('Ctrl Pts',(-1.83861259533635,-3.52885529691004,5.87739687639672));
#2438=CARTESIAN_POINT('Ctrl Pts',(-1.8221693883486,-3.5317119505949,5.87301471768675));
#2439=CARTESIAN_POINT('Ctrl Pts',(-1.8031965360398,-3.5325292633732,5.86571767937469));
#2440=CARTESIAN_POINT('Ctrl Pts',(-1.7978467878905,-3.53246960617574,5.86339641603733));
#2441=CARTESIAN_POINT('Ctrl Pts',(-1.78939267540214,-3.53128566216656,5.85871066493838));
#2442=CARTESIAN_POINT('Ctrl Pts',(-1.78573164524593,-3.53035794931988,5.85629392382858));
#2443=CARTESIAN_POINT('Ctrl Pts',(-1.78291230217384,-3.5287119654385,5.85355339059329));
#2444=CARTESIAN_POINT('',(-3.23003245950903,-2.27979707930028,5.85355339059283));
#2445=CARTESIAN_POINT('Ctrl Pts',(-3.23003245950903,-2.27979707930028,5.85355339059283));
#2446=CARTESIAN_POINT('Ctrl Pts',(-3.06237060858304,-2.53028665703206,5.86101811512799));
#2447=CARTESIAN_POINT('Ctrl Pts',(-2.8672692603167,-2.75973624708032,5.86778388571594));
#2448=CARTESIAN_POINT('Ctrl Pts',(-2.42798671078865,-3.17234364110549,5.88125347566854));
#2449=CARTESIAN_POINT('Ctrl Pts',(-2.18560986572065,-3.35359023328628,5.8879969490314));
#2450=CARTESIAN_POINT('Ctrl Pts',(-1.92533487773279,-3.50614968428127,5.89456992403025));
#2451=CARTESIAN_POINT('Origin',(0.,0.,5.85355339059327));
#2452=CARTESIAN_POINT('',(-4.30710678118655,-5.27468453316596E-16,6.));
#2453=CARTESIAN_POINT('Origin',(-4.30710678118655,-5.27468453316596E-16,
5.5));
#2454=CARTESIAN_POINT('Origin',(0.,0.,6.));
#2455=CARTESIAN_POINT('Origin',(0.,0.,0.5));
#2456=CARTESIAN_POINT('',(-4.30710678118655,-5.27468453316597E-16,0.));
#2457=CARTESIAN_POINT('Origin',(0.,0.,0.));
#2458=CARTESIAN_POINT('',(-3.95355339059327,-4.84170650504822E-16,0.146446609406728));
#2459=CARTESIAN_POINT('Origin',(-4.30710678118655,-5.27468453316597E-16,
0.5));
#2460=CARTESIAN_POINT('',(3.8670348623328,0.822572662914562,0.146446609406718));
#2461=CARTESIAN_POINT('Origin',(0.,0.,0.146446609406727));
#2462=CARTESIAN_POINT('',(3.88127665353657,0.967311500351366,0.105430075969749));
#2463=CARTESIAN_POINT('Ctrl Pts',(3.88127665353656,0.967311500351366,0.105430075969749));
#2464=CARTESIAN_POINT('Ctrl Pts',(3.88248308853003,0.942624045074989,0.109165675612358));
#2465=CARTESIAN_POINT('Ctrl Pts',(3.88301386655303,0.91577332765413,0.11376015133996));
#2466=CARTESIAN_POINT('Ctrl Pts',(3.88125811584264,0.87695729052849,0.122614170727277));
#2467=CARTESIAN_POINT('Ctrl Pts',(3.87986047067845,0.86016035953523,0.12699679547179));
#2468=CARTESIAN_POINT('Ctrl Pts',(3.87585665541296,0.841420755760116,0.134285593835466));
#2469=CARTESIAN_POINT('Ctrl Pts',(3.87444654520301,0.836203179878026,0.136606342515798));
#2470=CARTESIAN_POINT('Ctrl Pts',(3.87116677266274,0.828250561618554,0.141286175182243));
#2471=CARTESIAN_POINT('Ctrl Pts',(3.86934405717525,0.824905655118957,0.143702548179272));
#2472=CARTESIAN_POINT('Ctrl Pts',(3.8670348623328,0.822572662914562,0.14644660940672));
#2473=CARTESIAN_POINT('',(3.06184528645475,2.50113731212209,0.146446609406361));
#2474=CARTESIAN_POINT('Ctrl Pts',(3.06184528645475,2.50113731212209,0.146446609406361));
#2475=CARTESIAN_POINT('Ctrl Pts',(3.25229900237144,2.27922540622542,0.139337140594871));
#2476=CARTESIAN_POINT('Ctrl Pts',(3.4178992421145,2.03712868284477,0.132251957017881));
#2477=CARTESIAN_POINT('Ctrl Pts',(3.69349621819754,1.52125455462991,0.118447746003577));
#2478=CARTESIAN_POINT('Ctrl Pts',(3.80267865496227,1.24900013388164,0.11176958286899));
#2479=CARTESIAN_POINT('Ctrl Pts',(3.88127665353657,0.967311500351366,0.105430075969749));
#2480=CARTESIAN_POINT('Origin',(0.,0.,0.146446609406727));
#2481=CARTESIAN_POINT('Origin',(0.,0.,5.3));
#2482=CARTESIAN_POINT('Ctrl Pts',(-3.23003245950872,-2.27979707930074,5.85355339059284));
#2483=CARTESIAN_POINT('Ctrl Pts',(-3.48605757216865,-1.89729132736786,5.8421545128545));
#2484=CARTESIAN_POINT('Ctrl Pts',(-3.67290272589447,-1.47278615773723,5.83034317876559));
#2485=CARTESIAN_POINT('Ctrl Pts',(-3.90198272549636,-0.534286906649729,
5.80580144893728));
#2486=CARTESIAN_POINT('Ctrl Pts',(-3.92678469732619,-0.02095778682808,5.79389770355618));
#2487=CARTESIAN_POINT('Ctrl Pts',(-3.81417632172746,0.728069662839366,5.77501120790831));
#2488=CARTESIAN_POINT('Ctrl Pts',(-3.7531401911908,0.970805272996208,5.76861936561077));
#2489=CARTESIAN_POINT('Ctrl Pts',(-3.50475866615656,1.66529912267685,5.74950565622732));
#2490=CARTESIAN_POINT('Ctrl Pts',(-3.25470781791685,2.08932025578728,5.73673040142659));
#2491=CARTESIAN_POINT('Ctrl Pts',(-2.76729357820159,2.64262507560001,5.71826865242523));
#2492=CARTESIAN_POINT('Ctrl Pts',(-2.58350558298145,2.81460592309003,5.7122710989614));
#2493=CARTESIAN_POINT('Ctrl Pts',(-2.18871662021604,3.11566208020901,5.69970279956277));
#2494=CARTESIAN_POINT('Ctrl Pts',(-1.97971756236558,3.24500780490607,5.69331974913885));
#2495=CARTESIAN_POINT('Ctrl Pts',(-1.32932365492135,3.5647148010959,5.67419034251822));
#2496=CARTESIAN_POINT('Ctrl Pts',(-0.862609493406725,3.69236352207214,5.66136219147516));
#2497=CARTESIAN_POINT('Ctrl Pts',(-0.141997420183257,3.74802113639565,5.64282043347147));
#2498=CARTESIAN_POINT('Ctrl Pts',(0.103704543707698,3.74343271684464,5.63684833894108));
#2499=CARTESIAN_POINT('Ctrl Pts',(0.808078967993443,3.65931037385989,5.61861265296486));
#2500=CARTESIAN_POINT('Ctrl Pts',(1.25466121318322,3.51794596391685,5.60603376474256));
#2501=CARTESIAN_POINT('Ctrl Pts',(1.87377897388947,3.1843067039061,5.5869756032409));
#2502=CARTESIAN_POINT('Ctrl Pts',(2.07267489777189,3.05081927368397,5.58054440091542));
#2503=CARTESIAN_POINT('Ctrl Pts',(2.62925119655528,2.59340895698975,5.56157229450649));
#2504=CARTESIAN_POINT('Ctrl Pts',(2.93852342211069,2.21760690130707,5.54955345539839));
#2505=CARTESIAN_POINT('Ctrl Pts',(3.38505687577488,1.37528752962112,5.52343629412718));
#2506=CARTESIAN_POINT('Ctrl Pts',(3.52229264131942,0.921136157090413,5.51030337752685));
#2507=CARTESIAN_POINT('Ctrl Pts',(3.61579848004809,-0.0158981524309145,
5.48495880691041));
#2508=CARTESIAN_POINT('Ctrl Pts',(3.57061186396643,-0.490757310244434,5.47293902065656));
#2509=CARTESIAN_POINT('Ctrl Pts',(3.29802269785456,-1.38356055051093,5.44682324267042));
#2510=CARTESIAN_POINT('Ctrl Pts',(3.07950407722148,-1.793017386471,5.43369601743825));
#2511=CARTESIAN_POINT('Ctrl Pts',(2.49700735160396,-2.50729774012675,5.40833391065028));
#2512=CARTESIAN_POINT('Ctrl Pts',(2.13732363548428,-2.80556135170051,5.39631287055879));
#2513=CARTESIAN_POINT('Ctrl Pts',(1.33146390865158,-3.23596187835134,5.37019862528225));
#2514=CARTESIAN_POINT('Ctrl Pts',(0.897477746127028,-3.36866325812721,5.35707701665436));
#2515=CARTESIAN_POINT('Ctrl Pts',(0.184867188647294,-3.44228476569018,5.33691297012429));
#2516=CARTESIAN_POINT('Ctrl Pts',(-0.0852040363592367,-3.43924476673309,
5.32978546915416));
#2517=CARTESIAN_POINT('Ctrl Pts',(-0.606244419702814,-3.37055296824439,
5.31501529318569));
#2518=CARTESIAN_POINT('Ctrl Pts',(-0.856073829920963,-3.30823594612872,
5.30756035389141));
#2519=CARTESIAN_POINT('Ctrl Pts',(-1.09648221583289,-3.21834223636364,5.29999999999999));
#2520=CARTESIAN_POINT('Ctrl Pts',(-1.78291230217383,-3.52871196543852,5.85355339059329));
#2521=CARTESIAN_POINT('Ctrl Pts',(-1.65032523775131,-3.45130522020063,5.72467256717835));
#2522=CARTESIAN_POINT('Ctrl Pts',(-1.52284260312185,-3.36708660390191,5.59465869876949));
#2523=CARTESIAN_POINT('Ctrl Pts',(-1.40116082960876,-3.27654653614685,5.46356687519203));
#2524=CARTESIAN_POINT('Ctrl Pts',(-1.35072296474922,-3.23901710532119,5.40922848505441));
#2525=CARTESIAN_POINT('Ctrl Pts',(-1.30128192586066,-3.20040211538145,5.35470488551682));
#2526=CARTESIAN_POINT('Ctrl Pts',(-1.25288796387014,-3.16073911450935,5.3));
#2527=CARTESIAN_POINT('Origin',(0.,0.,0.));
#2528=CARTESIAN_POINT('Ctrl Pts',(3.06184528645506,2.50113731212173,0.146446609406349));
#2529=CARTESIAN_POINT('Ctrl Pts',(2.77435240222989,2.8361168296548,0.15717846456648));
#2530=CARTESIAN_POINT('Ctrl Pts',(2.43294573365056,3.12119414411317,0.167440655963785));
#2531=CARTESIAN_POINT('Ctrl Pts',(1.6853369919954,3.5539312966052,0.189277673693473));
#2532=CARTESIAN_POINT('Ctrl Pts',(1.28936104917625,3.70449697040217,0.200164930942241));
#2533=CARTESIAN_POINT('Ctrl Pts',(0.414742223530389,3.88361747138701,0.222891527846362));
#2534=CARTESIAN_POINT('Ctrl Pts',(-0.102681428720145,3.90226753828496,0.234832426921827));
#2535=CARTESIAN_POINT('Ctrl Pts',(-1.1281484694038,3.70272941302675,0.261366829194983));
#2536=CARTESIAN_POINT('Ctrl Pts',(-1.59371735193676,3.51313738339041,0.274524268420465));
#2537=CARTESIAN_POINT('Ctrl Pts',(-2.39606359536181,2.98601592969997,0.299463936486715));
#2538=CARTESIAN_POINT('Ctrl Pts',(-2.76812379329783,2.64148334326332,0.311401996056597));
#2539=CARTESIAN_POINT('Ctrl Pts',(-3.20456765415488,1.9976794673569,0.331543524760906));
#2540=CARTESIAN_POINT('Ctrl Pts',(-3.32080929617615,1.78433802431732,0.337962163790949));
#2541=CARTESIAN_POINT('Ctrl Pts',(-3.60018016321903,1.12728340083744,0.357030647934769));
#2542=CARTESIAN_POINT('Ctrl Pts',(-3.70120939598955,0.66235242669122,0.369666669227658));
#2543=CARTESIAN_POINT('Ctrl Pts',(-3.71971832458559,-0.0514672817840994,
0.387829343601874));
#2544=CARTESIAN_POINT('Ctrl Pts',(-3.70248187722653,-0.293585158448379,
0.393850398705496));
#2545=CARTESIAN_POINT('Ctrl Pts',(-3.5819983306588,-0.991762845935543,0.41248195793184));
#2546=CARTESIAN_POINT('Ctrl Pts',(-3.41639083385021,-1.43124925906229,0.42526125755466));
#2547=CARTESIAN_POINT('Ctrl Pts',(-2.9216272443319,-2.23850002061275,0.450991006289752));
#2548=CARTESIAN_POINT('Ctrl Pts',(-2.58993108590179,-2.59866365023318,0.463093178436547));
#2549=CARTESIAN_POINT('Ctrl Pts',(-1.8288152789984,-3.14755490593119,0.488216083183662));
#2550=CARTESIAN_POINT('Ctrl Pts',(-1.41283102553677,-3.3412129182102,0.500953731458646));
#2551=CARTESIAN_POINT('Ctrl Pts',(-0.514426264589624,-3.56737174753317,
0.526698120079665));
#2552=CARTESIAN_POINT('Ctrl Pts',(-0.035457866608088,-3.59227952289105,
0.5388576269144));
#2553=CARTESIAN_POINT('Ctrl Pts',(0.871840240219401,-3.45560228292562,0.563867472849291));
#2554=CARTESIAN_POINT('Ctrl Pts',(1.29449180806901,-3.30695688143785,0.57655861188009));
#2555=CARTESIAN_POINT('Ctrl Pts',(1.87507805263777,-2.96922557851636,0.595651996080249));
#2556=CARTESIAN_POINT('Ctrl Pts',(2.06025795852984,-2.83596564228176,0.602058454826432));
#2557=CARTESIAN_POINT('Ctrl Pts',(2.40416549124293,-2.53391662692938,0.614625275375867));
#2558=CARTESIAN_POINT('Ctrl Pts',(2.56306026431644,-2.36433530990857,0.620688671243676));
#2559=CARTESIAN_POINT('Ctrl Pts',(2.96597110497598,-1.8352358126166,0.639127980815));
#2560=CARTESIAN_POINT('Ctrl Pts',(3.16100735459105,-1.44424233619295,0.651755137766466));
#2561=CARTESIAN_POINT('Ctrl Pts',(3.33449176366876,-0.828384328578818,0.670371247269878));
#2562=CARTESIAN_POINT('Ctrl Pts',(3.37251101126901,-0.624749332251278,0.676341748573088));
#2563=CARTESIAN_POINT('Ctrl Pts',(3.41216803127686,-0.206693409248142,0.688226656305019));
#2564=CARTESIAN_POINT('Ctrl Pts',(3.41272231692649,0.00880057830198792,
0.694005688511974));
#2565=CARTESIAN_POINT('Ctrl Pts',(3.39272377138046,0.222318265353878,0.700000000000002));
#2566=CARTESIAN_POINT('Ctrl Pts',(3.8670348623328,0.822572662914563,0.146446609406718));
#2567=CARTESIAN_POINT('Ctrl Pts',(3.77302895909947,0.727597983697717,0.25815565598544));
#2568=CARTESIAN_POINT('Ctrl Pts',(3.67519496548545,0.637291809812134,0.370594064843146));
#2569=CARTESIAN_POINT('Ctrl Pts',(3.5738640727637,0.552046912101368,0.483750533529002));
#2570=CARTESIAN_POINT('Ctrl Pts',(3.50957206027576,0.497961076272375,0.555545589335125));
#2571=CARTESIAN_POINT('Ctrl Pts',(3.44387284612637,0.445913479209334,0.627629707095193));
#2572=CARTESIAN_POINT('Ctrl Pts',(3.37685862035149,0.396012446973337,0.700000000000002));
#2573=CARTESIAN_POINT('Origin',(0.,0.,0.));
#2574=CARTESIAN_POINT('',(3.46410161513774,-6.,0.700000000000016));
#2575=CARTESIAN_POINT('',(6.92820323027547,-5.50774703622636E-14,0.7));
#2576=CARTESIAN_POINT('Ctrl Pts',(3.46410161513143,-6.00000000001093,0.700000000003416));
#2577=CARTESIAN_POINT('Ctrl Pts',(5.19615242270661,-3.00000000000003,-0.232642742539615));
#2578=CARTESIAN_POINT('Ctrl Pts',(6.92820323028178,1.08718214755315E-11,
0.700000000003399));
#2579=CARTESIAN_POINT('',(-3.46410161513767,-6.00000000000001,0.7));
#2580=CARTESIAN_POINT('Ctrl Pts',(-3.46410161515028,-6.00000000000001,0.700000000003395));
#2581=CARTESIAN_POINT('Ctrl Pts',(3.30846461338297E-14,-6.,-0.232642742539606));
#2582=CARTESIAN_POINT('Ctrl Pts',(3.46410161515036,-6.,0.700000000003413));
#2583=CARTESIAN_POINT('',(-6.92820323027547,-1.26634813746307E-13,0.7));
#2584=CARTESIAN_POINT('Ctrl Pts',(-6.92820323028178,1.07991580485185E-11,
0.700000000003397));
#2585=CARTESIAN_POINT('Ctrl Pts',(-5.19615242270662,-3.00000000000007,-0.23264274253959));
#2586=CARTESIAN_POINT('Ctrl Pts',(-3.46410161513145,-6.00000000001097,0.700000000003437));
#2587=CARTESIAN_POINT('',(-5.62820323027547,-6.89256107090765E-16,0.));
#2588=CARTESIAN_POINT('',(-3.46410161513784,5.99999999999991,0.7));
#2589=CARTESIAN_POINT('Ctrl Pts',(-3.46410161513153,6.00000000001084,0.700000000003399));
#2590=CARTESIAN_POINT('Ctrl Pts',(-5.19615242270669,2.99999999999995,-0.232642742539597));
#2591=CARTESIAN_POINT('Ctrl Pts',(-6.92820323028188,-1.09821184038314E-11,
0.70000000000345));
#2592=CARTESIAN_POINT('',(3.46410161513769,6.,0.7));
#2593=CARTESIAN_POINT('Ctrl Pts',(3.46410161515031,6.,0.700000000003399));
#2594=CARTESIAN_POINT('Ctrl Pts',(-4.9960036108132E-14,6.,-0.232642742539617));
#2595=CARTESIAN_POINT('Ctrl Pts',(-3.46410161515044,6.,0.700000000003435));
#2596=CARTESIAN_POINT('Ctrl Pts',(6.92820323028178,-1.09842486020173E-11,
0.700000000003399));
#2597=CARTESIAN_POINT('Ctrl Pts',(5.19615242270659,2.99999999999997,-0.232642742539654));
#2598=CARTESIAN_POINT('Ctrl Pts',(3.46410161513139,6.00000000001092,0.700000000003399));
#2599=CARTESIAN_POINT('Origin',(0.,0.,5.3));
#2600=CARTESIAN_POINT('',(-3.46410161513778,-6.00000000000001,5.29999999999997));
#2601=CARTESIAN_POINT('',(-6.92820323027547,-1.26634813746307E-13,5.3));
#2602=CARTESIAN_POINT('Ctrl Pts',(-3.46410161512789,-6.00000000001713,5.29999999999465));
#2603=CARTESIAN_POINT('Ctrl Pts',(-5.19615242270664,-3.00000000000005,6.23264274254104));
#2604=CARTESIAN_POINT('Ctrl Pts',(-6.92820323028537,1.70112774321325E-11,
5.29999999999467));
#2605=CARTESIAN_POINT('',(3.46410161513769,-6.,5.3));
#2606=CARTESIAN_POINT('Ctrl Pts',(3.46410161515748,-6.,5.29999999999467));
#2607=CARTESIAN_POINT('Ctrl Pts',(-3.06421554796543E-14,-6.,6.23264274254106));
#2608=CARTESIAN_POINT('Ctrl Pts',(-3.46410161515757,-6.,5.29999999999464));
#2609=CARTESIAN_POINT('',(6.92820323027547,-5.50774703622636E-14,5.3));
#2610=CARTESIAN_POINT('Ctrl Pts',(6.92820323028536,1.70703849372499E-11,
5.29999999999468));
#2611=CARTESIAN_POINT('Ctrl Pts',(5.19615242270661,-3.00000000000003,6.23264274254106));
#2612=CARTESIAN_POINT('Ctrl Pts',(3.46410161512784,-6.00000000001715,5.29999999999465));
#2613=CARTESIAN_POINT('',(6.92820323027547,-8.48460190979921E-16,5.3));
#2614=CARTESIAN_POINT('',(3.46410161513769,6.,5.3));
#2615=CARTESIAN_POINT('Ctrl Pts',(3.4641016151278,6.00000000001713,5.29999999999467));
#2616=CARTESIAN_POINT('Ctrl Pts',(5.19615242270659,2.99999999999997,6.2326427425411));
#2617=CARTESIAN_POINT('Ctrl Pts',(6.92820323028537,-1.72005130880512E-11,
5.29999999999467));
#2618=CARTESIAN_POINT('',(-3.46410161513784,5.99999999999991,5.3));
#2619=CARTESIAN_POINT('Ctrl Pts',(-3.46410161515761,6.,5.29999999999464));
#2620=CARTESIAN_POINT('Ctrl Pts',(-4.9737991503207E-14,6.,6.23264274254107));
#2621=CARTESIAN_POINT('Ctrl Pts',(3.46410161515748,6.,5.29999999999467));
#2622=CARTESIAN_POINT('Ctrl Pts',(-6.92820323028547,-1.71902036394844E-11,
5.29999999999462));
#2623=CARTESIAN_POINT('Ctrl Pts',(-5.19615242270669,2.99999999999995,6.23264274254104));
#2624=CARTESIAN_POINT('Ctrl Pts',(-3.46410161512795,6.00000000001704,5.29999999999467));
#2625=CARTESIAN_POINT('Origin',(0.,0.,6.));
#2626=CARTESIAN_POINT('Ctrl Pts',(3.4,-4.1286418728248E-14,4.4275));
#2627=CARTESIAN_POINT('Ctrl Pts',(3.4,-0.186121573168501,4.41717515564813));
#2628=CARTESIAN_POINT('Ctrl Pts',(3.38471908137672,-0.372333688940097,4.40649416451766));
#2629=CARTESIAN_POINT('Ctrl Pts',(3.28124216860171,-0.995696340847217,4.36953627202487));
#2630=CARTESIAN_POINT('Ctrl Pts',(3.12293048658518,-1.41606837879289,4.34257902116854));
#2631=CARTESIAN_POINT('Ctrl Pts',(2.65619550095441,-2.16746765440165,4.2901715462705));
#2632=CARTESIAN_POINT('Ctrl Pts',(2.35399859648627,-2.49238497036037,4.26644003600835));
#2633=CARTESIAN_POINT('Ctrl Pts',(1.63859104158029,-3.01209070895768,4.21481199464172));
#2634=CARTESIAN_POINT('Ctrl Pts',(1.23110761644009,-3.20031628743618,4.18788236252099));
#2635=CARTESIAN_POINT('Ctrl Pts',(0.371201765949229,-3.40821037856945,4.13540326192926));
#2636=CARTESIAN_POINT('Ctrl Pts',(-0.0725687904280879,-3.42759737449122,
4.11160847464233));
#2637=CARTESIAN_POINT('Ctrl Pts',(-0.94703531002039,-3.29552875407992,4.06006395368984));
#2638=CARTESIAN_POINT('Ctrl Pts',(-1.36908596543482,-3.14371830215661,4.0331629686661));
#2639=CARTESIAN_POINT('Ctrl Pts',(-2.12770774344354,-2.688300844554,3.98061488863892));
#2640=CARTESIAN_POINT('Ctrl Pts',(-2.45775731231282,-2.39029937611201,3.95674944530396));
#2641=CARTESIAN_POINT('Ctrl Pts',(-2.98785764954916,-1.68220467166189,3.90528822802077));
#2642=CARTESIAN_POINT('Ctrl Pts',(-3.18174475294303,-1.27811503245704,3.87841677143123));
#2643=CARTESIAN_POINT('Ctrl Pts',(-3.40252747310172,-0.421110543648273,
3.82580246582334));
#2644=CARTESIAN_POINT('Ctrl Pts',(-3.4284082411663,0.0233109517265578,3.8018596191488));
#2645=CARTESIAN_POINT('Ctrl Pts',(-3.30863368964708,0.899875278664372,3.75048121754253));
#2646=CARTESIAN_POINT('Ctrl Pts',(-3.16311132282504,1.32345283364206,3.72364001706537));
#2647=CARTESIAN_POINT('Ctrl Pts',(-2.71867737003119,2.08896069354698,3.67096231921887));
#2648=CARTESIAN_POINT('Ctrl Pts',(-2.42473352762095,2.42396950470071,3.64693600787735));
#2649=CARTESIAN_POINT('Ctrl Pts',(-1.72372676814348,2.96400603940907,3.59563967146296));
#2650=CARTESIAN_POINT('Ctrl Pts',(-1.32296629343995,3.16327215273327,3.56882929723005));
#2651=CARTESIAN_POINT('Ctrl Pts',(-0.468845437377404,3.39640865728536,3.51609109274558));
#2652=CARTESIAN_POINT('Ctrl Pts',(-0.0238015395680562,3.42853269676147,
3.49197598107518));
#2653=CARTESIAN_POINT('Ctrl Pts',(0.854691311762255,3.3205134009099,3.44076070874106));
#2654=CARTESIAN_POINT('Ctrl Pts',(1.27964077780986,3.18100414093045,3.41398157215478));
#2655=CARTESIAN_POINT('Ctrl Pts',(2.05164359087632,2.74711062423187,3.36118577302349));
#2656=CARTESIAN_POINT('Ctrl Pts',(2.39139213819153,2.45704990197379,3.33697727616224));
#2657=CARTESIAN_POINT('Ctrl Pts',(2.94082692627242,1.76283634079008,3.2858418307883));
#2658=CARTESIAN_POINT('Ctrl Pts',(3.14514957850475,1.36530114858836,3.25909418591775));
#2659=CARTESIAN_POINT('Ctrl Pts',(3.35557986947541,0.633683454545388,3.21367342189199));
#2660=CARTESIAN_POINT('Ctrl Pts',(3.40000000000004,0.317340779883098,3.19510405364632));
#2661=CARTESIAN_POINT('Ctrl Pts',(3.4,-4.57203719328447E-13,3.17749999999997));
#2662=CARTESIAN_POINT('Ctrl Pts',(3.4,4.02367417807767E-13,3.18750000000002));
#2663=CARTESIAN_POINT('Ctrl Pts',(3.4,0.084778075557853,3.19220294990359));
#2664=CARTESIAN_POINT('Ctrl Pts',(3.39682921836388,0.169643165693244,3.19698358485793));
#2665=CARTESIAN_POINT('Ctrl Pts',(3.35666479179104,0.704885329940955,3.22759832104023));
#2666=CARTESIAN_POINT('Ctrl Pts',(3.23342729542556,1.14409166058361,3.25479444641897));
#2667=CARTESIAN_POINT('Ctrl Pts',(2.82979832555493,1.93447068967886,3.30791422448257));
#2668=CARTESIAN_POINT('Ctrl Pts',(2.55882097173626,2.2808604668407,3.33233732015604));
#2669=CARTESIAN_POINT('Ctrl Pts',(1.888689857903,2.86305918557583,3.38288967177184));
#2670=CARTESIAN_POINT('Ctrl Pts',(1.49184515045318,3.0884605724715,3.41008335885311));
#2671=CARTESIAN_POINT('Ctrl Pts',(0.648567420366776,3.36590927212086,3.46323825849629));
#2672=CARTESIAN_POINT('Ctrl Pts',(0.212215696658642,3.42124204383506,3.48773952075238));
#2673=CARTESIAN_POINT('Ctrl Pts',(-0.673844997879645,3.36309030641018,3.5382287552024));
#2674=CARTESIAN_POINT('Ctrl Pts',(-1.11458071880527,3.24377623285994,3.56541956927481));
#2675=CARTESIAN_POINT('Ctrl Pts',(-1.90903929904592,2.84703508925413,3.61860738689352));
#2676=CARTESIAN_POINT('Ctrl Pts',(-2.25793303097117,2.57909280652053,3.64318594206919));
#2677=CARTESIAN_POINT('Ctrl Pts',(-2.84640735314467,1.91378832788541,3.69361474302511));
#2678=CARTESIAN_POINT('Ctrl Pts',(-3.07546706131234,1.5185689169317,3.72080232965667));
#2679=CARTESIAN_POINT('Ctrl Pts',(-3.36028375995725,0.677194277000098,3.77402095937644));
#2680=CARTESIAN_POINT('Ctrl Pts',(-3.41933581790506,0.241198415149406,3.79867554450871));
#2681=CARTESIAN_POINT('Ctrl Pts',(-3.36863576566522,-0.645818691105451,
3.84904661023061));
#2682=CARTESIAN_POINT('Ctrl Pts',(-3.25287263204456,-1.08790383774031,3.87623068859344));
#2683=CARTESIAN_POINT('Ctrl Pts',(-2.86235949762462,-1.88601685512811,3.92947812437708));
#2684=CARTESIAN_POINT('Ctrl Pts',(-2.59714842325084,-2.23716566450476,3.95420713965067));
#2685=CARTESIAN_POINT('Ctrl Pts',(-1.93620626854934,-2.83126355461424,4.00452316455724));
#2686=CARTESIAN_POINT('Ctrl Pts',(-1.54247446483059,-3.06359998871188,4.03170352059063));
#2687=CARTESIAN_POINT('Ctrl Pts',(-0.702836250273089,-3.35503314843299,
4.08497785709781));
#2688=CARTESIAN_POINT('Ctrl Pts',(-0.267158441261753,-3.41742225278365,
4.10977941670543));
#2689=CARTESIAN_POINT('Ctrl Pts',(0.620689477376828,-3.37340234046731,4.16004307476651));
#2690=CARTESIAN_POINT('Ctrl Pts',(1.06395928212342,-3.26082992394206,4.18721955433763));
#2691=CARTESIAN_POINT('Ctrl Pts',(1.86532592317619,-2.87590884056273,4.24051898670533));
#2692=CARTESIAN_POINT('Ctrl Pts',(2.21849244667218,-2.61313980059034,4.26539096736468));
#2693=CARTESIAN_POINT('Ctrl Pts',(2.81759901065795,-1.95611272799177,4.31560489736237));
#2694=CARTESIAN_POINT('Ctrl Pts',(3.05285241159819,-1.5637307492961,4.34277739955764));
#2695=CARTESIAN_POINT('Ctrl Pts',(3.33394599822532,-0.771448153098491,4.39318716462197));
#2696=CARTESIAN_POINT('Ctrl Pts',(3.4,-0.386958995796732,4.41603396930755));
#2697=CARTESIAN_POINT('Ctrl Pts',(3.4,1.31769595235198E-13,4.43750000000001));
#2698=CARTESIAN_POINT('Origin',(0.,0.,6.));
#2699=CARTESIAN_POINT('Origin',(0.,0.,0.));
#2700=CARTESIAN_POINT('Origin',(3.46410161513774,-6.,6.));
#2701=CARTESIAN_POINT('',(3.46410161513774,-6.,6.));
#2702=CARTESIAN_POINT('',(6.92820323027547,-5.54031299473484E-14,6.));
#2703=CARTESIAN_POINT('Origin',(6.92820323027547,-5.54031299473484E-14,
6.));
#2704=CARTESIAN_POINT('',(3.4641016151377,6.,6.));
#2705=CARTESIAN_POINT('Origin',(3.4641016151377,6.,6.));
#2706=CARTESIAN_POINT('',(-3.46410161513779,6.,6.));
#2707=CARTESIAN_POINT('Origin',(-3.46410161513779,6.,6.));
#2708=CARTESIAN_POINT('',(-6.92820323027554,-6.46958707310266E-15,6.));
#2709=CARTESIAN_POINT('Origin',(-6.92820323027554,-6.46958707310266E-15,
6.));
#2710=CARTESIAN_POINT('',(-3.46410161513778,-6.00000000000001,6.));
#2711=CARTESIAN_POINT('Origin',(-3.46410161513778,-6.00000000000001,6.));
#2712=CARTESIAN_POINT('Ctrl Pts',(0.,3.4,6.));
#2713=CARTESIAN_POINT('Ctrl Pts',(1.40832611206852,3.4,5.921875));
#2714=CARTESIAN_POINT('Ctrl Pts',(2.40416305603426,2.40416305603426,5.84375));
#2715=CARTESIAN_POINT('Ctrl Pts',(3.4,1.40832611206852,5.765625));
#2716=CARTESIAN_POINT('Ctrl Pts',(3.4,2.0818995585505E-16,5.6875));
#2717=CARTESIAN_POINT('Ctrl Pts',(3.4,-1.40832611206852,5.609375));
#2718=CARTESIAN_POINT('Ctrl Pts',(2.40416305603426,-2.40416305603426,5.53125));
#2719=CARTESIAN_POINT('Ctrl Pts',(1.40832611206852,-3.4,5.453125));
#2720=CARTESIAN_POINT('Ctrl Pts',(4.163799117101E-16,-3.4,5.375));
#2721=CARTESIAN_POINT('Ctrl Pts',(-1.40832611206852,-3.4,5.296875));
#2722=CARTESIAN_POINT('Ctrl Pts',(-2.40416305603426,-2.40416305603426,5.21875));
#2723=CARTESIAN_POINT('Ctrl Pts',(-3.4,-1.40832611206853,5.140625));
#2724=CARTESIAN_POINT('Ctrl Pts',(-3.4,-6.2456986756515E-16,5.0625));
#2725=CARTESIAN_POINT('Ctrl Pts',(-3.4,1.40832611206852,4.984375));
#2726=CARTESIAN_POINT('Ctrl Pts',(-2.40416305603426,2.40416305603426,4.90625));
#2727=CARTESIAN_POINT('Ctrl Pts',(-1.40832611206853,3.4,4.828125));
#2728=CARTESIAN_POINT('Ctrl Pts',(0.,3.4,4.75));
#2729=CARTESIAN_POINT('Ctrl Pts',(1.40832611206852,3.4,4.671875));
#2730=CARTESIAN_POINT('Ctrl Pts',(2.40416305603426,2.40416305603426,4.59375));
#2731=CARTESIAN_POINT('Ctrl Pts',(3.4,1.40832611206852,4.515625));
#2732=CARTESIAN_POINT('Ctrl Pts',(3.4,2.0818995585505E-16,4.4375));
#2733=CARTESIAN_POINT('Ctrl Pts',(3.4,-1.40832611206852,4.359375));
#2734=CARTESIAN_POINT('Ctrl Pts',(2.40416305603426,-2.40416305603426,4.28125));
#2735=CARTESIAN_POINT('Ctrl Pts',(1.40832611206852,-3.4,4.203125));
#2736=CARTESIAN_POINT('Ctrl Pts',(4.163799117101E-16,-3.4,4.125));
#2737=CARTESIAN_POINT('Ctrl Pts',(-1.40832611206852,-3.4,4.046875));
#2738=CARTESIAN_POINT('Ctrl Pts',(-2.40416305603426,-2.40416305603426,3.96875));
#2739=CARTESIAN_POINT('Ctrl Pts',(-3.4,-1.40832611206853,3.890625));
#2740=CARTESIAN_POINT('Ctrl Pts',(-3.4,-6.2456986756515E-16,3.8125));
#2741=CARTESIAN_POINT('Ctrl Pts',(-3.4,1.40832611206852,3.734375));
#2742=CARTESIAN_POINT('Ctrl Pts',(-2.40416305603426,2.40416305603426,3.65625));
#2743=CARTESIAN_POINT('Ctrl Pts',(-1.40832611206853,3.4,3.578125));
#2744=CARTESIAN_POINT('Ctrl Pts',(0.,3.4,3.5));
#2745=CARTESIAN_POINT('Ctrl Pts',(1.40832611206852,3.4,3.421875));
#2746=CARTESIAN_POINT('Ctrl Pts',(2.40416305603426,2.40416305603426,3.34375));
#2747=CARTESIAN_POINT('Ctrl Pts',(3.4,1.40832611206852,3.265625));
#2748=CARTESIAN_POINT('Ctrl Pts',(3.4,2.0818995585505E-16,3.1875));
#2749=CARTESIAN_POINT('Ctrl Pts',(3.4,-1.40832611206852,3.109375));
#2750=CARTESIAN_POINT('Ctrl Pts',(2.40416305603426,-2.40416305603426,3.03125));
#2751=CARTESIAN_POINT('Ctrl Pts',(1.40832611206852,-3.4,2.953125));
#2752=CARTESIAN_POINT('Ctrl Pts',(4.163799117101E-16,-3.4,2.875));
#2753=CARTESIAN_POINT('Ctrl Pts',(-1.40832611206852,-3.4,2.796875));
#2754=CARTESIAN_POINT('Ctrl Pts',(-2.40416305603426,-2.40416305603426,2.71875));
#2755=CARTESIAN_POINT('Ctrl Pts',(-3.4,-1.40832611206853,2.640625));
#2756=CARTESIAN_POINT('Ctrl Pts',(-3.4,-6.2456986756515E-16,2.5625));
#2757=CARTESIAN_POINT('Ctrl Pts',(-3.4,1.40832611206852,2.484375));
#2758=CARTESIAN_POINT('Ctrl Pts',(-2.40416305603426,2.40416305603426,2.40625));
#2759=CARTESIAN_POINT('Ctrl Pts',(-1.40832611206853,3.4,2.328125));
#2760=CARTESIAN_POINT('Ctrl Pts',(0.,3.4,2.25));
#2761=CARTESIAN_POINT('Ctrl Pts',(1.40832611206852,3.4,2.171875));
#2762=CARTESIAN_POINT('Ctrl Pts',(2.40416305603426,2.40416305603426,2.09375));
#2763=CARTESIAN_POINT('Ctrl Pts',(3.4,1.40832611206852,2.015625));
#2764=CARTESIAN_POINT('Ctrl Pts',(3.4,2.0818995585505E-16,1.9375));
#2765=CARTESIAN_POINT('Ctrl Pts',(3.4,-1.40832611206852,1.859375));
#2766=CARTESIAN_POINT('Ctrl Pts',(2.40416305603426,-2.40416305603426,1.78125));
#2767=CARTESIAN_POINT('Ctrl Pts',(1.40832611206852,-3.4,1.703125));
#2768=CARTESIAN_POINT('Ctrl Pts',(4.163799117101E-16,-3.4,1.625));
#2769=CARTESIAN_POINT('Ctrl Pts',(-1.40832611206852,-3.4,1.546875));
#2770=CARTESIAN_POINT('Ctrl Pts',(-2.40416305603426,-2.40416305603426,1.46875));
#2771=CARTESIAN_POINT('Ctrl Pts',(-3.4,-1.40832611206853,1.390625));
#2772=CARTESIAN_POINT('Ctrl Pts',(-3.4,-6.2456986756515E-16,1.3125));
#2773=CARTESIAN_POINT('Ctrl Pts',(-3.4,1.40832611206852,1.234375));
#2774=CARTESIAN_POINT('Ctrl Pts',(-2.40416305603426,2.40416305603426,1.15625));
#2775=CARTESIAN_POINT('Ctrl Pts',(-1.40832611206853,3.4,1.078125));
#2776=CARTESIAN_POINT('Ctrl Pts',(0.,3.4,1.));
#2777=CARTESIAN_POINT('Ctrl Pts',(1.40832611206852,3.4,0.921875));
#2778=CARTESIAN_POINT('Ctrl Pts',(2.40416305603426,2.40416305603426,0.84375));
#2779=CARTESIAN_POINT('Ctrl Pts',(3.4,1.40832611206852,0.765625));
#2780=CARTESIAN_POINT('Ctrl Pts',(3.4,2.0818995585505E-16,0.6875));
#2781=CARTESIAN_POINT('Ctrl Pts',(3.4,-1.40832611206852,0.609375));
#2782=CARTESIAN_POINT('Ctrl Pts',(2.40416305603426,-2.40416305603426,0.53125));
#2783=CARTESIAN_POINT('Ctrl Pts',(1.40832611206852,-3.4,0.453125));
#2784=CARTESIAN_POINT('Ctrl Pts',(4.163799117101E-16,-3.4,0.375));
#2785=CARTESIAN_POINT('Ctrl Pts',(-1.40832611206852,-3.4,0.296875));
#2786=CARTESIAN_POINT('Ctrl Pts',(-2.40416305603426,-2.40416305603426,0.21875));
#2787=CARTESIAN_POINT('Ctrl Pts',(-3.4,-1.40832611206853,0.140625));
#2788=CARTESIAN_POINT('Ctrl Pts',(-3.4,-6.2456986756515E-16,0.0625000000000001));
#2789=CARTESIAN_POINT('Ctrl Pts',(-3.4,1.40832611206852,-0.015625));
#2790=CARTESIAN_POINT('Ctrl Pts',(-2.40416305603426,2.40416305603426,-0.0937500000000001));
#2791=CARTESIAN_POINT('Ctrl Pts',(-1.40832611206853,3.4,-0.171875));
#2792=CARTESIAN_POINT('Ctrl Pts',(0.,3.4,-0.25));
#2793=CARTESIAN_POINT('Ctrl Pts',(1.40832611206852,3.4,-0.328125));
#2794=CARTESIAN_POINT('Ctrl Pts',(2.40416305603426,2.40416305603426,-0.40625));
#2795=CARTESIAN_POINT('Ctrl Pts',(3.4,1.40832611206852,-0.484375));
#2796=CARTESIAN_POINT('Ctrl Pts',(3.4,2.0818995585505E-16,-0.5625));
#2797=CARTESIAN_POINT('Ctrl Pts',(3.4,-1.40832611206852,-0.640625));
#2798=CARTESIAN_POINT('Ctrl Pts',(2.40416305603426,-2.40416305603426,-0.71875));
#2799=CARTESIAN_POINT('Ctrl Pts',(1.40832611206852,-3.4,-0.796875));
#2800=CARTESIAN_POINT('Ctrl Pts',(4.163799117101E-16,-3.4,-0.875));
#2801=CARTESIAN_POINT('Ctrl Pts',(-1.40832611206852,-3.4,-0.953125));
#2802=CARTESIAN_POINT('Ctrl Pts',(-2.40416305603426,-2.40416305603426,-1.03125));
#2803=CARTESIAN_POINT('Ctrl Pts',(-3.4,-1.40832611206853,-1.109375));
#2804=CARTESIAN_POINT('Ctrl Pts',(-3.4,-6.2456986756515E-16,-1.1875));
#2805=CARTESIAN_POINT('Ctrl Pts',(-3.4,1.40832611206852,-1.265625));
#2806=CARTESIAN_POINT('Ctrl Pts',(-2.40416305603426,2.40416305603426,-1.34375));
#2807=CARTESIAN_POINT('Ctrl Pts',(-1.40832611206853,3.4,-1.421875));
#2808=CARTESIAN_POINT('Ctrl Pts',(0.,3.4,-1.5));
#2809=CARTESIAN_POINT('Ctrl Pts',(0.,4.,6.62));
#2810=CARTESIAN_POINT('Ctrl Pts',(1.65685424949238,4.,6.541875));
#2811=CARTESIAN_POINT('Ctrl Pts',(2.82842712474619,2.82842712474619,6.46375));
#2812=CARTESIAN_POINT('Ctrl Pts',(4.,1.65685424949238,6.385625));
#2813=CARTESIAN_POINT('Ctrl Pts',(4.,2.44929359829471E-16,6.3075));
#2814=CARTESIAN_POINT('Ctrl Pts',(4.,-1.65685424949238,6.229375));
#2815=CARTESIAN_POINT('Ctrl Pts',(2.82842712474619,-2.82842712474619,6.15125));
#2816=CARTESIAN_POINT('Ctrl Pts',(1.65685424949238,-4.,6.073125));
#2817=CARTESIAN_POINT('Ctrl Pts',(4.89858719658941E-16,-4.,5.995));
#2818=CARTESIAN_POINT('Ctrl Pts',(-1.65685424949238,-4.,5.916875));
#2819=CARTESIAN_POINT('Ctrl Pts',(-2.82842712474619,-2.82842712474619,5.83875));
#2820=CARTESIAN_POINT('Ctrl Pts',(-4.,-1.65685424949238,5.760625));
#2821=CARTESIAN_POINT('Ctrl Pts',(-4.,-7.34788079488412E-16,5.6825));
#2822=CARTESIAN_POINT('Ctrl Pts',(-4.,1.65685424949238,5.604375));
#2823=CARTESIAN_POINT('Ctrl Pts',(-2.82842712474619,2.82842712474619,5.52625));
#2824=CARTESIAN_POINT('Ctrl Pts',(-1.65685424949238,4.,5.448125));
#2825=CARTESIAN_POINT('Ctrl Pts',(0.,4.,5.37));
#2826=CARTESIAN_POINT('Ctrl Pts',(1.65685424949238,4.,5.291875));
#2827=CARTESIAN_POINT('Ctrl Pts',(2.82842712474619,2.82842712474619,5.21375));
#2828=CARTESIAN_POINT('Ctrl Pts',(4.,1.65685424949238,5.135625));
#2829=CARTESIAN_POINT('Ctrl Pts',(4.,2.44929359829471E-16,5.0575));
#2830=CARTESIAN_POINT('Ctrl Pts',(4.,-1.65685424949238,4.979375));
#2831=CARTESIAN_POINT('Ctrl Pts',(2.82842712474619,-2.82842712474619,4.90125));
#2832=CARTESIAN_POINT('Ctrl Pts',(1.65685424949238,-4.,4.823125));
#2833=CARTESIAN_POINT('Ctrl Pts',(4.89858719658941E-16,-4.,4.745));
#2834=CARTESIAN_POINT('Ctrl Pts',(-1.65685424949238,-4.,4.666875));
#2835=CARTESIAN_POINT('Ctrl Pts',(-2.82842712474619,-2.82842712474619,4.58875));
#2836=CARTESIAN_POINT('Ctrl Pts',(-4.,-1.65685424949238,4.510625));
#2837=CARTESIAN_POINT('Ctrl Pts',(-4.,-7.34788079488412E-16,4.4325));
#2838=CARTESIAN_POINT('Ctrl Pts',(-4.,1.65685424949238,4.354375));
#2839=CARTESIAN_POINT('Ctrl Pts',(-2.82842712474619,2.82842712474619,4.27625));
#2840=CARTESIAN_POINT('Ctrl Pts',(-1.65685424949238,4.,4.198125));
#2841=CARTESIAN_POINT('Ctrl Pts',(0.,4.,4.12));
#2842=CARTESIAN_POINT('Ctrl Pts',(1.65685424949238,4.,4.041875));
#2843=CARTESIAN_POINT('Ctrl Pts',(2.82842712474619,2.82842712474619,3.96375));
#2844=CARTESIAN_POINT('Ctrl Pts',(4.,1.65685424949238,3.885625));
#2845=CARTESIAN_POINT('Ctrl Pts',(4.,2.44929359829471E-16,3.8075));
#2846=CARTESIAN_POINT('Ctrl Pts',(4.,-1.65685424949238,3.729375));
#2847=CARTESIAN_POINT('Ctrl Pts',(2.82842712474619,-2.82842712474619,3.65125));
#2848=CARTESIAN_POINT('Ctrl Pts',(1.65685424949238,-4.,3.573125));
#2849=CARTESIAN_POINT('Ctrl Pts',(4.89858719658941E-16,-4.,3.495));
#2850=CARTESIAN_POINT('Ctrl Pts',(-1.65685424949238,-4.,3.416875));
#2851=CARTESIAN_POINT('Ctrl Pts',(-2.82842712474619,-2.82842712474619,3.33875));
#2852=CARTESIAN_POINT('Ctrl Pts',(-4.,-1.65685424949238,3.260625));
#2853=CARTESIAN_POINT('Ctrl Pts',(-4.,-7.34788079488412E-16,3.1825));
#2854=CARTESIAN_POINT('Ctrl Pts',(-4.,1.65685424949238,3.104375));
#2855=CARTESIAN_POINT('Ctrl Pts',(-2.82842712474619,2.82842712474619,3.02625));
#2856=CARTESIAN_POINT('Ctrl Pts',(-1.65685424949238,4.,2.948125));
#2857=CARTESIAN_POINT('Ctrl Pts',(0.,4.,2.87));
#2858=CARTESIAN_POINT('Ctrl Pts',(1.65685424949238,4.,2.791875));
#2859=CARTESIAN_POINT('Ctrl Pts',(2.82842712474619,2.82842712474619,2.71375));
#2860=CARTESIAN_POINT('Ctrl Pts',(4.,1.65685424949238,2.635625));
#2861=CARTESIAN_POINT('Ctrl Pts',(4.,2.44929359829471E-16,2.5575));
#2862=CARTESIAN_POINT('Ctrl Pts',(4.,-1.65685424949238,2.479375));
#2863=CARTESIAN_POINT('Ctrl Pts',(2.82842712474619,-2.82842712474619,2.40125));
#2864=CARTESIAN_POINT('Ctrl Pts',(1.65685424949238,-4.,2.323125));
#2865=CARTESIAN_POINT('Ctrl Pts',(4.89858719658941E-16,-4.,2.245));
#2866=CARTESIAN_POINT('Ctrl Pts',(-1.65685424949238,-4.,2.166875));
#2867=CARTESIAN_POINT('Ctrl Pts',(-2.82842712474619,-2.82842712474619,2.08875));
#2868=CARTESIAN_POINT('Ctrl Pts',(-4.,-1.65685424949238,2.010625));
#2869=CARTESIAN_POINT('Ctrl Pts',(-4.,-7.34788079488412E-16,1.9325));
#2870=CARTESIAN_POINT('Ctrl Pts',(-4.,1.65685424949238,1.854375));
#2871=CARTESIAN_POINT('Ctrl Pts',(-2.82842712474619,2.82842712474619,1.77625));
#2872=CARTESIAN_POINT('Ctrl Pts',(-1.65685424949238,4.,1.698125));
#2873=CARTESIAN_POINT('Ctrl Pts',(0.,4.,1.62));
#2874=CARTESIAN_POINT('Ctrl Pts',(1.65685424949238,4.,1.541875));
#2875=CARTESIAN_POINT('Ctrl Pts',(2.82842712474619,2.82842712474619,1.46375));
#2876=CARTESIAN_POINT('Ctrl Pts',(4.,1.65685424949238,1.385625));
#2877=CARTESIAN_POINT('Ctrl Pts',(4.,2.44929359829471E-16,1.3075));
#2878=CARTESIAN_POINT('Ctrl Pts',(4.,-1.65685424949238,1.229375));
#2879=CARTESIAN_POINT('Ctrl Pts',(2.82842712474619,-2.82842712474619,1.15125));
#2880=CARTESIAN_POINT('Ctrl Pts',(1.65685424949238,-4.,1.073125));
#2881=CARTESIAN_POINT('Ctrl Pts',(4.89858719658941E-16,-4.,0.995));
#2882=CARTESIAN_POINT('Ctrl Pts',(-1.65685424949238,-4.,0.916875));
#2883=CARTESIAN_POINT('Ctrl Pts',(-2.82842712474619,-2.82842712474619,0.83875));
#2884=CARTESIAN_POINT('Ctrl Pts',(-4.,-1.65685424949238,0.760625));
#2885=CARTESIAN_POINT('Ctrl Pts',(-4.,-7.34788079488412E-16,0.6825));
#2886=CARTESIAN_POINT('Ctrl Pts',(-4.,1.65685424949238,0.604375));
#2887=CARTESIAN_POINT('Ctrl Pts',(-2.82842712474619,2.82842712474619,0.52625));
#2888=CARTESIAN_POINT('Ctrl Pts',(-1.65685424949238,4.,0.448125));
#2889=CARTESIAN_POINT('Ctrl Pts',(0.,4.,0.37));
#2890=CARTESIAN_POINT('Ctrl Pts',(1.65685424949238,4.,0.291875));
#2891=CARTESIAN_POINT('Ctrl Pts',(2.82842712474619,2.82842712474619,0.21375));
#2892=CARTESIAN_POINT('Ctrl Pts',(4.,1.65685424949238,0.135624999999999));
#2893=CARTESIAN_POINT('Ctrl Pts',(4.,2.44929359829471E-16,0.0575000000000003));
#2894=CARTESIAN_POINT('Ctrl Pts',(4.,-1.65685424949238,-0.0206249999999998));
#2895=CARTESIAN_POINT('Ctrl Pts',(2.82842712474619,-2.82842712474619,-0.0987499999999999));
#2896=CARTESIAN_POINT('Ctrl Pts',(1.65685424949238,-4.,-0.176875));
#2897=CARTESIAN_POINT('Ctrl Pts',(4.89858719658941E-16,-4.,-0.255));
#2898=CARTESIAN_POINT('Ctrl Pts',(-1.65685424949238,-4.,-0.333125));
#2899=CARTESIAN_POINT('Ctrl Pts',(-2.82842712474619,-2.82842712474619,-0.41125));
#2900=CARTESIAN_POINT('Ctrl Pts',(-4.,-1.65685424949238,-0.489375));
#2901=CARTESIAN_POINT('Ctrl Pts',(-4.,-7.34788079488412E-16,-0.5675));
#2902=CARTESIAN_POINT('Ctrl Pts',(-4.,1.65685424949238,-0.645625000000001));
#2903=CARTESIAN_POINT('Ctrl Pts',(-2.82842712474619,2.82842712474619,-0.723750000000001));
#2904=CARTESIAN_POINT('Ctrl Pts',(-1.65685424949238,4.,-0.801875000000001));
#2905=CARTESIAN_POINT('Ctrl Pts',(0.,4.,-0.88));
#2906=CARTESIAN_POINT('Ctrl Pts',(-1.92533487773279,-3.50614968428127,5.89456992403025));
#2907=CARTESIAN_POINT('Ctrl Pts',(-2.42519093634574,-3.23166331314664,5.86563934498587));
#2908=CARTESIAN_POINT('Ctrl Pts',(-2.82842712474619,-2.82842712474619,5.83875));
#2909=CARTESIAN_POINT('Ctrl Pts',(-4.,-1.65685424949238,5.760625));
#2910=CARTESIAN_POINT('Ctrl Pts',(-4.,-7.34788079488412E-16,5.6825));
#2911=CARTESIAN_POINT('Ctrl Pts',(-4.,1.65685424949238,5.604375));
#2912=CARTESIAN_POINT('Ctrl Pts',(-2.82842712474619,2.82842712474619,5.52625));
#2913=CARTESIAN_POINT('Ctrl Pts',(-1.65685424949238,4.,5.448125));
#2914=CARTESIAN_POINT('Ctrl Pts',(0.,4.,5.37));
#2915=CARTESIAN_POINT('Ctrl Pts',(1.65685424949238,4.,5.291875));
#2916=CARTESIAN_POINT('Ctrl Pts',(2.82842712474619,2.82842712474619,5.21375));
#2917=CARTESIAN_POINT('Ctrl Pts',(4.,1.65685424949238,5.135625));
#2918=CARTESIAN_POINT('Ctrl Pts',(4.,2.44929359829471E-16,5.0575));
#2919=CARTESIAN_POINT('Ctrl Pts',(4.,-1.65685424949238,4.979375));
#2920=CARTESIAN_POINT('Ctrl Pts',(2.82842712474619,-2.82842712474619,4.90125));
#2921=CARTESIAN_POINT('Ctrl Pts',(1.65685424949238,-4.,4.823125));
#2922=CARTESIAN_POINT('Ctrl Pts',(4.89858719658941E-16,-4.,4.745));
#2923=CARTESIAN_POINT('Ctrl Pts',(-1.65685424949238,-4.,4.666875));
#2924=CARTESIAN_POINT('Ctrl Pts',(-2.82842712474619,-2.82842712474619,4.58875));
#2925=CARTESIAN_POINT('Ctrl Pts',(-4.,-1.65685424949238,4.510625));
#2926=CARTESIAN_POINT('Ctrl Pts',(-4.,-7.34788079488412E-16,4.4325));
#2927=CARTESIAN_POINT('Ctrl Pts',(-4.,1.65685424949238,4.354375));
#2928=CARTESIAN_POINT('Ctrl Pts',(-2.82842712474619,2.82842712474619,4.27625));
#2929=CARTESIAN_POINT('Ctrl Pts',(-1.65685424949238,4.,4.198125));
#2930=CARTESIAN_POINT('Ctrl Pts',(0.,4.,4.12));
#2931=CARTESIAN_POINT('Ctrl Pts',(1.65685424949238,4.,4.041875));
#2932=CARTESIAN_POINT('Ctrl Pts',(2.82842712474619,2.82842712474619,3.96375));
#2933=CARTESIAN_POINT('Ctrl Pts',(4.,1.65685424949238,3.885625));
#2934=CARTESIAN_POINT('Ctrl Pts',(4.,2.44929359829471E-16,3.8075));
#2935=CARTESIAN_POINT('Ctrl Pts',(4.,-1.65685424949238,3.729375));
#2936=CARTESIAN_POINT('Ctrl Pts',(2.82842712474619,-2.82842712474619,3.65125));
#2937=CARTESIAN_POINT('Ctrl Pts',(1.65685424949238,-4.,3.573125));
#2938=CARTESIAN_POINT('Ctrl Pts',(4.89858719658941E-16,-4.,3.495));
#2939=CARTESIAN_POINT('Ctrl Pts',(-1.65685424949238,-4.,3.416875));
#2940=CARTESIAN_POINT('Ctrl Pts',(-2.82842712474619,-2.82842712474619,3.33875));
#2941=CARTESIAN_POINT('Ctrl Pts',(-4.,-1.65685424949238,3.260625));
#2942=CARTESIAN_POINT('Ctrl Pts',(-4.,-7.34788079488412E-16,3.1825));
#2943=CARTESIAN_POINT('Ctrl Pts',(-4.,1.65685424949238,3.104375));
#2944=CARTESIAN_POINT('Ctrl Pts',(-2.82842712474619,2.82842712474619,3.02625));
#2945=CARTESIAN_POINT('Ctrl Pts',(-1.65685424949238,4.,2.948125));
#2946=CARTESIAN_POINT('Ctrl Pts',(0.,4.,2.87));
#2947=CARTESIAN_POINT('Ctrl Pts',(1.65685424949238,4.,2.791875));
#2948=CARTESIAN_POINT('Ctrl Pts',(2.82842712474619,2.82842712474619,2.71375));
#2949=CARTESIAN_POINT('Ctrl Pts',(4.,1.65685424949238,2.635625));
#2950=CARTESIAN_POINT('Ctrl Pts',(4.,2.44929359829471E-16,2.5575));
#2951=CARTESIAN_POINT('Ctrl Pts',(4.,-1.65685424949238,2.479375));
#2952=CARTESIAN_POINT('Ctrl Pts',(2.82842712474619,-2.82842712474619,2.40125));
#2953=CARTESIAN_POINT('Ctrl Pts',(1.65685424949238,-4.,2.323125));
#2954=CARTESIAN_POINT('Ctrl Pts',(4.89858719658941E-16,-4.,2.245));
#2955=CARTESIAN_POINT('Ctrl Pts',(-1.65685424949238,-4.,2.166875));
#2956=CARTESIAN_POINT('Ctrl Pts',(-2.82842712474619,-2.82842712474619,2.08875));
#2957=CARTESIAN_POINT('Ctrl Pts',(-4.,-1.65685424949238,2.010625));
#2958=CARTESIAN_POINT('Ctrl Pts',(-4.,-7.34788079488412E-16,1.9325));
#2959=CARTESIAN_POINT('Ctrl Pts',(-4.,1.65685424949238,1.854375));
#2960=CARTESIAN_POINT('Ctrl Pts',(-2.82842712474619,2.82842712474619,1.77625));
#2961=CARTESIAN_POINT('Ctrl Pts',(-1.65685424949238,4.,1.698125));
#2962=CARTESIAN_POINT('Ctrl Pts',(0.,4.,1.62));
#2963=CARTESIAN_POINT('Ctrl Pts',(1.65685424949238,4.,1.541875));
#2964=CARTESIAN_POINT('Ctrl Pts',(2.82842712474619,2.82842712474619,1.46375));
#2965=CARTESIAN_POINT('Ctrl Pts',(4.,1.65685424949238,1.385625));
#2966=CARTESIAN_POINT('Ctrl Pts',(4.,2.44929359829471E-16,1.3075));
#2967=CARTESIAN_POINT('Ctrl Pts',(4.,-1.65685424949238,1.229375));
#2968=CARTESIAN_POINT('Ctrl Pts',(2.82842712474619,-2.82842712474619,1.15125));
#2969=CARTESIAN_POINT('Ctrl Pts',(1.65685424949238,-4.,1.073125));
#2970=CARTESIAN_POINT('Ctrl Pts',(4.89858719658941E-16,-4.,0.995));
#2971=CARTESIAN_POINT('Ctrl Pts',(-1.65685424949238,-4.,0.916875));
#2972=CARTESIAN_POINT('Ctrl Pts',(-2.82842712474619,-2.82842712474619,0.83875));
#2973=CARTESIAN_POINT('Ctrl Pts',(-4.,-1.65685424949238,0.760625));
#2974=CARTESIAN_POINT('Ctrl Pts',(-4.,-7.34788079488412E-16,0.6825));
#2975=CARTESIAN_POINT('Ctrl Pts',(-4.,1.65685424949238,0.604375));
#2976=CARTESIAN_POINT('Ctrl Pts',(-2.82842712474619,2.82842712474619,0.52625));
#2977=CARTESIAN_POINT('Ctrl Pts',(-1.65685424949238,4.,0.448125));
#2978=CARTESIAN_POINT('Ctrl Pts',(0.,4.,0.37));
#2979=CARTESIAN_POINT('Ctrl Pts',(1.65685424949238,4.,0.291875));
#2980=CARTESIAN_POINT('Ctrl Pts',(2.82842712474619,2.82842712474619,0.21375));
#2981=CARTESIAN_POINT('Ctrl Pts',(3.6129669626084,2.04388728688398,0.161433856354469));
#2982=CARTESIAN_POINT('Ctrl Pts',(3.88127665353657,0.967311500351366,0.105430075969749));
#2983=CARTESIAN_POINT('Ctrl Pts',(0.,4.,6.62));
#2984=CARTESIAN_POINT('Ctrl Pts',(1.65685424949238,4.,6.541875));
#2985=CARTESIAN_POINT('Ctrl Pts',(2.82842712474619,2.82842712474619,6.46375));
#2986=CARTESIAN_POINT('Ctrl Pts',(4.,1.65685424949238,6.385625));
#2987=CARTESIAN_POINT('Ctrl Pts',(4.,2.44929359829471E-16,6.3075));
#2988=CARTESIAN_POINT('Ctrl Pts',(4.,-1.65685424949238,6.229375));
#2989=CARTESIAN_POINT('Ctrl Pts',(2.82842712474619,-2.82842712474619,6.15125));
#2990=CARTESIAN_POINT('Ctrl Pts',(1.65685424949238,-4.,6.073125));
#2991=CARTESIAN_POINT('Ctrl Pts',(4.89858719658941E-16,-4.,5.995));
#2992=CARTESIAN_POINT('Ctrl Pts',(-1.65685424949238,-4.,5.916875));
#2993=CARTESIAN_POINT('Ctrl Pts',(-2.82842712474619,-2.82842712474619,5.83875));
#2994=CARTESIAN_POINT('Ctrl Pts',(-4.,-1.65685424949238,5.760625));
#2995=CARTESIAN_POINT('Ctrl Pts',(-4.,-7.34788079488412E-16,5.6825));
#2996=CARTESIAN_POINT('Ctrl Pts',(-4.,1.65685424949238,5.604375));
#2997=CARTESIAN_POINT('Ctrl Pts',(-2.82842712474619,2.82842712474619,5.52625));
#2998=CARTESIAN_POINT('Ctrl Pts',(-1.65685424949238,4.,5.448125));
#2999=CARTESIAN_POINT('Ctrl Pts',(0.,4.,5.37));
#3000=CARTESIAN_POINT('Ctrl Pts',(1.65685424949238,4.,5.291875));
#3001=CARTESIAN_POINT('Ctrl Pts',(2.82842712474619,2.82842712474619,5.21375));
#3002=CARTESIAN_POINT('Ctrl Pts',(4.,1.65685424949238,5.135625));
#3003=CARTESIAN_POINT('Ctrl Pts',(4.,2.44929359829471E-16,5.0575));
#3004=CARTESIAN_POINT('Ctrl Pts',(4.,-1.65685424949238,4.979375));
#3005=CARTESIAN_POINT('Ctrl Pts',(2.82842712474619,-2.82842712474619,4.90125));
#3006=CARTESIAN_POINT('Ctrl Pts',(1.65685424949238,-4.,4.823125));
#3007=CARTESIAN_POINT('Ctrl Pts',(4.89858719658941E-16,-4.,4.745));
#3008=CARTESIAN_POINT('Ctrl Pts',(-1.65685424949238,-4.,4.666875));
#3009=CARTESIAN_POINT('Ctrl Pts',(-2.82842712474619,-2.82842712474619,4.58875));
#3010=CARTESIAN_POINT('Ctrl Pts',(-4.,-1.65685424949238,4.510625));
#3011=CARTESIAN_POINT('Ctrl Pts',(-4.,-7.34788079488412E-16,4.4325));
#3012=CARTESIAN_POINT('Ctrl Pts',(-4.,1.65685424949238,4.354375));
#3013=CARTESIAN_POINT('Ctrl Pts',(-2.82842712474619,2.82842712474619,4.27625));
#3014=CARTESIAN_POINT('Ctrl Pts',(-1.65685424949238,4.,4.198125));
#3015=CARTESIAN_POINT('Ctrl Pts',(0.,4.,4.12));
#3016=CARTESIAN_POINT('Ctrl Pts',(1.65685424949238,4.,4.041875));
#3017=CARTESIAN_POINT('Ctrl Pts',(2.82842712474619,2.82842712474619,3.96375));
#3018=CARTESIAN_POINT('Ctrl Pts',(4.,1.65685424949238,3.885625));
#3019=CARTESIAN_POINT('Ctrl Pts',(4.,2.44929359829471E-16,3.8075));
#3020=CARTESIAN_POINT('Ctrl Pts',(4.,-1.65685424949238,3.729375));
#3021=CARTESIAN_POINT('Ctrl Pts',(2.82842712474619,-2.82842712474619,3.65125));
#3022=CARTESIAN_POINT('Ctrl Pts',(1.65685424949238,-4.,3.573125));
#3023=CARTESIAN_POINT('Ctrl Pts',(4.89858719658941E-16,-4.,3.495));
#3024=CARTESIAN_POINT('Ctrl Pts',(-1.65685424949238,-4.,3.416875));
#3025=CARTESIAN_POINT('Ctrl Pts',(-2.82842712474619,-2.82842712474619,3.33875));
#3026=CARTESIAN_POINT('Ctrl Pts',(-4.,-1.65685424949238,3.260625));
#3027=CARTESIAN_POINT('Ctrl Pts',(-4.,-7.34788079488412E-16,3.1825));
#3028=CARTESIAN_POINT('Ctrl Pts',(-4.,1.65685424949238,3.104375));
#3029=CARTESIAN_POINT('Ctrl Pts',(-2.82842712474619,2.82842712474619,3.02625));
#3030=CARTESIAN_POINT('Ctrl Pts',(-1.65685424949238,4.,2.948125));
#3031=CARTESIAN_POINT('Ctrl Pts',(0.,4.,2.87));
#3032=CARTESIAN_POINT('Ctrl Pts',(1.65685424949238,4.,2.791875));
#3033=CARTESIAN_POINT('Ctrl Pts',(2.82842712474619,2.82842712474619,2.71375));
#3034=CARTESIAN_POINT('Ctrl Pts',(4.,1.65685424949238,2.635625));
#3035=CARTESIAN_POINT('Ctrl Pts',(4.,2.44929359829471E-16,2.5575));
#3036=CARTESIAN_POINT('Ctrl Pts',(4.,-1.65685424949238,2.479375));
#3037=CARTESIAN_POINT('Ctrl Pts',(2.82842712474619,-2.82842712474619,2.40125));
#3038=CARTESIAN_POINT('Ctrl Pts',(1.65685424949238,-4.,2.323125));
#3039=CARTESIAN_POINT('Ctrl Pts',(4.89858719658941E-16,-4.,2.245));
#3040=CARTESIAN_POINT('Ctrl Pts',(-1.65685424949238,-4.,2.166875));
#3041=CARTESIAN_POINT('Ctrl Pts',(-2.82842712474619,-2.82842712474619,2.08875));
#3042=CARTESIAN_POINT('Ctrl Pts',(-4.,-1.65685424949238,2.010625));
#3043=CARTESIAN_POINT('Ctrl Pts',(-4.,-7.34788079488412E-16,1.9325));
#3044=CARTESIAN_POINT('Ctrl Pts',(-4.,1.65685424949238,1.854375));
#3045=CARTESIAN_POINT('Ctrl Pts',(-2.82842712474619,2.82842712474619,1.77625));
#3046=CARTESIAN_POINT('Ctrl Pts',(-1.65685424949238,4.,1.698125));
#3047=CARTESIAN_POINT('Ctrl Pts',(0.,4.,1.62));
#3048=CARTESIAN_POINT('Ctrl Pts',(1.65685424949238,4.,1.541875));
#3049=CARTESIAN_POINT('Ctrl Pts',(2.82842712474619,2.82842712474619,1.46375));
#3050=CARTESIAN_POINT('Ctrl Pts',(4.,1.65685424949238,1.385625));
#3051=CARTESIAN_POINT('Ctrl Pts',(4.,2.44929359829471E-16,1.3075));
#3052=CARTESIAN_POINT('Ctrl Pts',(4.,-1.65685424949238,1.229375));
#3053=CARTESIAN_POINT('Ctrl Pts',(2.82842712474619,-2.82842712474619,1.15125));
#3054=CARTESIAN_POINT('Ctrl Pts',(1.65685424949238,-4.,1.073125));
#3055=CARTESIAN_POINT('Ctrl Pts',(4.89858719658941E-16,-4.,0.995));
#3056=CARTESIAN_POINT('Ctrl Pts',(-1.65685424949238,-4.,0.916875));
#3057=CARTESIAN_POINT('Ctrl Pts',(-2.82842712474619,-2.82842712474619,0.83875));
#3058=CARTESIAN_POINT('Ctrl Pts',(-4.,-1.65685424949238,0.760625));
#3059=CARTESIAN_POINT('Ctrl Pts',(-4.,-7.34788079488412E-16,0.6825));
#3060=CARTESIAN_POINT('Ctrl Pts',(-4.,1.65685424949238,0.604375));
#3061=CARTESIAN_POINT('Ctrl Pts',(-2.82842712474619,2.82842712474619,0.52625));
#3062=CARTESIAN_POINT('Ctrl Pts',(-1.65685424949238,4.,0.448125));
#3063=CARTESIAN_POINT('Ctrl Pts',(0.,4.,0.37));
#3064=CARTESIAN_POINT('Ctrl Pts',(1.65685424949238,4.,0.291875));
#3065=CARTESIAN_POINT('Ctrl Pts',(2.82842712474619,2.82842712474619,0.21375));
#3066=CARTESIAN_POINT('Ctrl Pts',(4.,1.65685424949238,0.135624999999999));
#3067=CARTESIAN_POINT('Ctrl Pts',(4.,2.44929359829471E-16,0.0575000000000003));
#3068=CARTESIAN_POINT('Ctrl Pts',(4.,-1.65685424949238,-0.0206249999999998));
#3069=CARTESIAN_POINT('Ctrl Pts',(2.82842712474619,-2.82842712474619,-0.0987499999999999));
#3070=CARTESIAN_POINT('Ctrl Pts',(1.65685424949238,-4.,-0.176875));
#3071=CARTESIAN_POINT('Ctrl Pts',(4.89858719658941E-16,-4.,-0.255));
#3072=CARTESIAN_POINT('Ctrl Pts',(-1.65685424949238,-4.,-0.333125));
#3073=CARTESIAN_POINT('Ctrl Pts',(-2.82842712474619,-2.82842712474619,-0.41125));
#3074=CARTESIAN_POINT('Ctrl Pts',(-4.,-1.65685424949238,-0.489375));
#3075=CARTESIAN_POINT('Ctrl Pts',(-4.,-7.34788079488412E-16,-0.5675));
#3076=CARTESIAN_POINT('Ctrl Pts',(-4.,1.65685424949238,-0.645625000000001));
#3077=CARTESIAN_POINT('Ctrl Pts',(-2.82842712474619,2.82842712474619,-0.723750000000001));
#3078=CARTESIAN_POINT('Ctrl Pts',(-1.65685424949238,4.,-0.801875000000001));
#3079=CARTESIAN_POINT('Ctrl Pts',(0.,4.,-0.88));
#3080=CARTESIAN_POINT('Ctrl Pts',(0.,3.39995998131687,7.24004135263924));
#3081=CARTESIAN_POINT('Ctrl Pts',(1.40830953578722,3.39995998131687,7.16191635263924));
#3082=CARTESIAN_POINT('Ctrl Pts',(2.40413475855205,2.40413475855205,7.08379135263924));
#3083=CARTESIAN_POINT('Ctrl Pts',(3.39995998131687,1.40830953578722,7.00566635263924));
#3084=CARTESIAN_POINT('Ctrl Pts',(3.39995998131687,2.0818750541744E-16,
6.92754135263924));
#3085=CARTESIAN_POINT('Ctrl Pts',(3.39995998131687,-1.40830953578722,6.84941635263924));
#3086=CARTESIAN_POINT('Ctrl Pts',(2.40413475855205,-2.40413475855205,6.77129135263923));
#3087=CARTESIAN_POINT('Ctrl Pts',(1.40830953578722,-3.39995998131687,6.69316635263924));
#3088=CARTESIAN_POINT('Ctrl Pts',(4.1637501083488E-16,-3.39995998131687,
6.61504135263924));
#3089=CARTESIAN_POINT('Ctrl Pts',(-1.40830953578722,-3.39995998131687,6.53691635263924));
#3090=CARTESIAN_POINT('Ctrl Pts',(-2.40413475855205,-2.40413475855205,6.45879135263924));
#3091=CARTESIAN_POINT('Ctrl Pts',(-3.39995998131687,-1.40830953578722,6.38066635263924));
#3092=CARTESIAN_POINT('Ctrl Pts',(-3.39995998131687,-6.2456251625232E-16,
6.30254135263924));
#3093=CARTESIAN_POINT('Ctrl Pts',(-3.39995998131687,1.40830953578722,6.22441635263923));
#3094=CARTESIAN_POINT('Ctrl Pts',(-2.40413475855205,2.40413475855204,6.14629135263924));
#3095=CARTESIAN_POINT('Ctrl Pts',(-1.40830953578722,3.39995998131687,6.06816635263924));
#3096=CARTESIAN_POINT('Ctrl Pts',(0.,3.39995998131687,5.99004135263923));
#3097=CARTESIAN_POINT('Ctrl Pts',(1.40830953578722,3.39995998131687,5.91191635263923));
#3098=CARTESIAN_POINT('Ctrl Pts',(2.40413475855205,2.40413475855205,5.83379135263924));
#3099=CARTESIAN_POINT('Ctrl Pts',(3.39995998131687,1.40830953578722,5.75566635263924));
#3100=CARTESIAN_POINT('Ctrl Pts',(3.39995998131687,2.0818750541744E-16,
5.67754135263924));
#3101=CARTESIAN_POINT('Ctrl Pts',(3.39995998131687,-1.40830953578722,5.59941635263924));
#3102=CARTESIAN_POINT('Ctrl Pts',(2.40413475855205,-2.40413475855205,5.52129135263924));
#3103=CARTESIAN_POINT('Ctrl Pts',(1.40830953578722,-3.39995998131687,5.44316635263924));
#3104=CARTESIAN_POINT('Ctrl Pts',(4.1637501083488E-16,-3.39995998131687,
5.36504135263924));
#3105=CARTESIAN_POINT('Ctrl Pts',(-1.40830953578722,-3.39995998131687,5.28691635263924));
#3106=CARTESIAN_POINT('Ctrl Pts',(-2.40413475855205,-2.40413475855205,5.20879135263924));
#3107=CARTESIAN_POINT('Ctrl Pts',(-3.39995998131687,-1.40830953578722,5.13066635263924));
#3108=CARTESIAN_POINT('Ctrl Pts',(-3.39995998131687,-6.2456251625232E-16,
5.05254135263924));
#3109=CARTESIAN_POINT('Ctrl Pts',(-3.39995998131687,1.40830953578722,4.97441635263923));
#3110=CARTESIAN_POINT('Ctrl Pts',(-2.40413475855205,2.40413475855204,4.89629135263924));
#3111=CARTESIAN_POINT('Ctrl Pts',(-1.40830953578722,3.39995998131687,4.81816635263924));
#3112=CARTESIAN_POINT('Ctrl Pts',(0.,3.39995998131687,4.74004135263923));
#3113=CARTESIAN_POINT('Ctrl Pts',(1.40830953578722,3.39995998131687,4.66191635263923));
#3114=CARTESIAN_POINT('Ctrl Pts',(2.40413475855205,2.40413475855205,4.58379135263924));
#3115=CARTESIAN_POINT('Ctrl Pts',(3.39995998131687,1.40830953578722,4.50566635263923));
#3116=CARTESIAN_POINT('Ctrl Pts',(3.39995998131687,2.0818750541744E-16,
4.42754135263924));
#3117=CARTESIAN_POINT('Ctrl Pts',(3.39995998131687,-1.40830953578722,4.34941635263924));
#3118=CARTESIAN_POINT('Ctrl Pts',(2.40413475855205,-2.40413475855205,4.27129135263924));
#3119=CARTESIAN_POINT('Ctrl Pts',(1.40830953578722,-3.39995998131687,4.19316635263924));
#3120=CARTESIAN_POINT('Ctrl Pts',(4.1637501083488E-16,-3.39995998131687,
4.11504135263923));
#3121=CARTESIAN_POINT('Ctrl Pts',(-1.40830953578722,-3.39995998131687,4.03691635263924));
#3122=CARTESIAN_POINT('Ctrl Pts',(-2.40413475855205,-2.40413475855205,3.95879135263924));
#3123=CARTESIAN_POINT('Ctrl Pts',(-3.39995998131687,-1.40830953578722,3.88066635263924));
#3124=CARTESIAN_POINT('Ctrl Pts',(-3.39995998131687,-6.2456251625232E-16,
3.80254135263923));
#3125=CARTESIAN_POINT('Ctrl Pts',(-3.39995998131687,1.40830953578722,3.72441635263924));
#3126=CARTESIAN_POINT('Ctrl Pts',(-2.40413475855205,2.40413475855204,3.64629135263924));
#3127=CARTESIAN_POINT('Ctrl Pts',(-1.40830953578722,3.39995998131687,3.56816635263924));
#3128=CARTESIAN_POINT('Ctrl Pts',(0.,3.39995998131687,3.49004135263924));
#3129=CARTESIAN_POINT('Ctrl Pts',(1.40830953578722,3.39995998131687,3.41191635263924));
#3130=CARTESIAN_POINT('Ctrl Pts',(2.40413475855205,2.40413475855205,3.33379135263924));
#3131=CARTESIAN_POINT('Ctrl Pts',(3.39995998131687,1.40830953578722,3.25566635263924));
#3132=CARTESIAN_POINT('Ctrl Pts',(3.39995998131687,2.0818750541744E-16,
3.17754135263923));
#3133=CARTESIAN_POINT('Ctrl Pts',(3.39995998131687,-1.40830953578722,3.09941635263924));
#3134=CARTESIAN_POINT('Ctrl Pts',(2.40413475855205,-2.40413475855205,3.02129135263924));
#3135=CARTESIAN_POINT('Ctrl Pts',(1.40830953578722,-3.39995998131687,2.94316635263924));
#3136=CARTESIAN_POINT('Ctrl Pts',(4.1637501083488E-16,-3.39995998131687,
2.86504135263923));
#3137=CARTESIAN_POINT('Ctrl Pts',(-1.40830953578722,-3.39995998131687,2.78691635263924));
#3138=CARTESIAN_POINT('Ctrl Pts',(-2.40413475855205,-2.40413475855205,2.70879135263924));
#3139=CARTESIAN_POINT('Ctrl Pts',(-3.39995998131687,-1.40830953578722,2.63066635263924));
#3140=CARTESIAN_POINT('Ctrl Pts',(-3.39995998131687,-6.2456251625232E-16,
2.55254135263924));
#3141=CARTESIAN_POINT('Ctrl Pts',(-3.39995998131687,1.40830953578722,2.47441635263924));
#3142=CARTESIAN_POINT('Ctrl Pts',(-2.40413475855205,2.40413475855204,2.39629135263924));
#3143=CARTESIAN_POINT('Ctrl Pts',(-1.40830953578722,3.39995998131687,2.31816635263924));
#3144=CARTESIAN_POINT('Ctrl Pts',(0.,3.39995998131687,2.24004135263924));
#3145=CARTESIAN_POINT('Ctrl Pts',(1.40830953578722,3.39995998131687,2.16191635263924));
#3146=CARTESIAN_POINT('Ctrl Pts',(2.40413475855205,2.40413475855205,2.08379135263924));
#3147=CARTESIAN_POINT('Ctrl Pts',(3.39995998131687,1.40830953578722,2.00566635263924));
#3148=CARTESIAN_POINT('Ctrl Pts',(3.39995998131687,2.0818750541744E-16,
1.92754135263924));
#3149=CARTESIAN_POINT('Ctrl Pts',(3.39995998131687,-1.40830953578722,1.84941635263924));
#3150=CARTESIAN_POINT('Ctrl Pts',(2.40413475855205,-2.40413475855205,1.77129135263924));
#3151=CARTESIAN_POINT('Ctrl Pts',(1.40830953578722,-3.39995998131687,1.69316635263924));
#3152=CARTESIAN_POINT('Ctrl Pts',(4.1637501083488E-16,-3.39995998131687,
1.61504135263924));
#3153=CARTESIAN_POINT('Ctrl Pts',(-1.40830953578722,-3.39995998131687,1.53691635263924));
#3154=CARTESIAN_POINT('Ctrl Pts',(-2.40413475855205,-2.40413475855205,1.45879135263924));
#3155=CARTESIAN_POINT('Ctrl Pts',(-3.39995998131687,-1.40830953578722,1.38066635263924));
#3156=CARTESIAN_POINT('Ctrl Pts',(-3.39995998131687,-6.2456251625232E-16,
1.30254135263924));
#3157=CARTESIAN_POINT('Ctrl Pts',(-3.39995998131687,1.40830953578722,1.22441635263924));
#3158=CARTESIAN_POINT('Ctrl Pts',(-2.40413475855205,2.40413475855204,1.14629135263924));
#3159=CARTESIAN_POINT('Ctrl Pts',(-1.40830953578722,3.39995998131687,1.06816635263924));
#3160=CARTESIAN_POINT('Ctrl Pts',(0.,3.39995998131687,0.990041352639235));
#3161=CARTESIAN_POINT('Ctrl Pts',(1.40830953578722,3.39995998131687,0.911916352639235));
#3162=CARTESIAN_POINT('Ctrl Pts',(2.40413475855205,2.40413475855205,0.833791352639235));
#3163=CARTESIAN_POINT('Ctrl Pts',(3.39995998131687,1.40830953578722,0.755666352639235));
#3164=CARTESIAN_POINT('Ctrl Pts',(3.39995998131687,2.0818750541744E-16,
0.677541352639236));
#3165=CARTESIAN_POINT('Ctrl Pts',(3.39995998131687,-1.40830953578722,0.599416352639236));
#3166=CARTESIAN_POINT('Ctrl Pts',(2.40413475855205,-2.40413475855205,0.521291352639235));
#3167=CARTESIAN_POINT('Ctrl Pts',(1.40830953578722,-3.39995998131687,0.443166352639235));
#3168=CARTESIAN_POINT('Ctrl Pts',(4.1637501083488E-16,-3.39995998131687,
0.365041352639235));
#3169=CARTESIAN_POINT('Ctrl Pts',(-1.40830953578722,-3.39995998131687,0.286916352639235));
#3170=CARTESIAN_POINT('Ctrl Pts',(-2.40413475855205,-2.40413475855205,0.208791352639235));
#3171=CARTESIAN_POINT('Ctrl Pts',(-3.39995998131687,-1.40830953578722,0.130666352639235));
#3172=CARTESIAN_POINT('Ctrl Pts',(-3.39995998131687,-6.2456251625232E-16,
0.052541352639235));
#3173=CARTESIAN_POINT('Ctrl Pts',(-3.39995998131687,1.40830953578722,-0.0255836473607651));
#3174=CARTESIAN_POINT('Ctrl Pts',(-2.40413475855205,2.40413475855204,-0.103708647360765));
#3175=CARTESIAN_POINT('Ctrl Pts',(-1.40830953578722,3.39995998131687,-0.181833647360765));
#3176=CARTESIAN_POINT('Ctrl Pts',(0.,3.39995998131687,-0.259958647360764));
#3198=UNCERTAINTY_MEASURE_WITH_UNIT(LENGTH_MEASURE(0.01),#3208,
'DISTANCE_ACCURACY_VALUE',
'Maximum model space distance between geometric entities at asserted c
onnectivities');
#3199=UNCERTAINTY_MEASURE_WITH_UNIT(LENGTH_MEASURE(0.01),#3208,
'DISTANCE_ACCURACY_VALUE',
'Maximum model space distance between geometric entities at asserted c
onnectivities');
#3206=(
GEOMETRIC_REPRESENTATION_CONTEXT(3)
GLOBAL_UNCERTAINTY_ASSIGNED_CONTEXT((#3198))
GLOBAL_UNIT_ASSIGNED_CONTEXT((#3208,#3210,#3211))
REPRESENTATION_CONTEXT('','3D')
);
#3207=(
GEOMETRIC_REPRESENTATION_CONTEXT(3)
GLOBAL_UNCERTAINTY_ASSIGNED_CONTEXT((#3199))
GLOBAL_UNIT_ASSIGNED_CONTEXT((#3208,#3210,#3211))
REPRESENTATION_CONTEXT('','3D')
);
#3208=(
LENGTH_UNIT()
NAMED_UNIT(*)
SI_UNIT(.MILLI.,.METRE.)
);
#3210=(
NAMED_UNIT(*)
PLANE_ANGLE_UNIT()
SI_UNIT($,.RADIAN.)
);
#3211=(
NAMED_UNIT(*)
SI_UNIT($,.STERADIAN.)
SOLID_ANGLE_UNIT()
);
#3218=SHAPE_DEFINITION_REPRESENTATION(#3225,#3247);
#3225=PRODUCT_DEFINITION_SHAPE('',$,#3255);
#3247=SHAPE_REPRESENTATION('',(#1465),#3206);
#3248=PRODUCT_DEFINITION_CONTEXT('part definition',#3271,'design');
#3255=PRODUCT_DEFINITION('Hex Nut DIN Grade C','Hex Nut DIN Grade C',#3262,
#3248);
#3262=PRODUCT_DEFINITION_FORMATION('',$,#3279);
#3271=APPLICATION_CONTEXT(
'Core Data for Automotive Mechanical Design Process');
#3272=PRODUCT_CONTEXT('part definition',#3271,'mechanical');
#3279=PRODUCT('Hex Nut DIN Grade C','Hex Nut DIN Grade C',$,(#3272));
#3283=PRESENTATION_STYLE_ASSIGNMENT((#3287));
#3287=SURFACE_STYLE_USAGE(.BOTH.,#3291);
#3291=SURFACE_SIDE_STYLE('',(#3295));
#3295=SURFACE_STYLE_FILL_AREA(#3299);
#3299=FILL_AREA_STYLE('Opaque(31,36,43)',(#3303));
#3303=FILL_AREA_STYLE_COLOUR('Opaque(31,36,43)',#3307);
#3307=COLOUR_RGB('Opaque(31,36,43)',0.12156862745098,0.141176470588235,
0.168627450980392);
ENDSEC;
END-ISO-10303-21;
